ISO-10303-21;
HEADER;
FILE_DESCRIPTION (('STEP AP214'),
    '1' );
FILE_NAME ('Snap Open Cable Crossbars 12.step',
    '2026-10-08T22:59:04',
    ( '' ),
    ( '' ),
    'SwSTEP 2.0',
    'SolidWorks 2020',
    '' );
FILE_SCHEMA (( 'AUTOMOTIVE_DESIGN' ));
ENDSEC;

DATA;
#61=CARTESIAN_POINT ( 'NONE',  ( -18.39418127959864790, 64.51609439831406689, -145.7731074845244450 ) ) ;
#146=LINE ( 'NONE', #4012, #142490 ) ;
#195=EDGE_CURVE ( 'NONE', #225539, #67597, #120326, .T. ) ;
#459=CARTESIAN_POINT ( 'NONE',  ( -16.77779411440718249, 66.05389855290464141, -149.1861649015289402 ) ) ;
#541=CARTESIAN_POINT ( 'NONE',  ( -16.97683809663753962, 66.05000000001226113, -149.7946366524138284 ) ) ;
#651=DIRECTION ( 'NONE',  ( 1.000000000000000000, 0.000000000000000000, 0.000000000000000000 ) ) ;
#892=ORIENTED_EDGE ( 'NONE', *, *, #60521, .F. ) ;
#958=CARTESIAN_POINT ( 'NONE',  ( -16.94052228080552425, 66.01372026691339556, -149.1327319818550450 ) ) ;
#969=VECTOR ( 'NONE', #242743, 1000.000000000000000 ) ;
#1142=CARTESIAN_POINT ( 'NONE',  ( -16.94445028196808778, 66.00793639031455484, -157.4157773061059800 ) ) ;
#1245=CARTESIAN_POINT ( 'NONE',  ( -18.41431012584568805, 64.51252797080402956, -145.7498714714227788 ) ) ;
#1362=CIRCLE ( 'NONE', #196999, 0.1999999999999987899 ) ;
#1478=CARTESIAN_POINT ( 'NONE',  ( -17.04761207306819060, 65.97354912661452886, -157.3731074845244109 ) ) ;
#1532=ORIENTED_EDGE ( 'NONE', *, *, #65148, .F. ) ;
#1540=ORIENTED_EDGE ( 'NONE', *, *, #8391, .F. ) ;
#1623=EDGE_LOOP ( 'NONE', ( #42024, #102009, #184230, #237736 ) ) ;
#1895=ORIENTED_EDGE ( 'NONE', *, *, #207763, .F. ) ;
#1929=VECTOR ( 'NONE', #139704, 1000.000000000000000 ) ;
#1979=CARTESIAN_POINT ( 'NONE',  ( -16.93262454970419384, 65.99797953208187096, -149.0960312582870984 ) ) ;
#2008=VERTEX_POINT ( 'NONE', #231357 ) ;
#2070=EDGE_LOOP ( 'NONE', ( #17337, #64326, #202230, #204771 ) ) ;
#2155=ORIENTED_EDGE ( 'NONE', *, *, #13809, .F. ) ;
#2190=CARTESIAN_POINT ( 'NONE',  ( -18.34374000495059676, 64.52683809664972614, -145.7731074845244450 ) ) ;
#2201=ADVANCED_FACE ( 'NONE', ( #60393 ), #162094, .F. ) ;
#2287=CARTESIAN_POINT ( 'NONE',  ( -18.40000000000000213, 64.52683809664972614, -145.7731074845244450 ) ) ;
#2329=PLANE ( 'NONE',  #252783 ) ;
#2350=EDGE_LOOP ( 'NONE', ( #67786, #198931, #110375, #253215 ) ) ;
#2395=CARTESIAN_POINT ( 'NONE',  ( -16.86733706339143879, 66.03400947037258106, -149.1199921825257206 ) ) ;
#2425=AXIS2_PLACEMENT_3D ( 'NONE', #153513, #135160, #16531 ) ;
#2751=PLANE ( 'NONE',  #12742 ) ;
#2890=CARTESIAN_POINT ( 'NONE',  ( -16.87683809663752399, 66.15000000001229807, -156.6207434663281219 ) ) ;
#2903=CARTESIAN_POINT ( 'NONE',  ( -18.40000000000000213, 64.52683809664972614, -145.8490535513323891 ) ) ;
#2931=( BOUNDED_CURVE ( )  B_SPLINE_CURVE ( 3, ( #2903, #124168, #27659, #186710 ),
 .UNSPECIFIED., .F., .F. ) 
 B_SPLINE_CURVE_WITH_KNOTS ( ( 4, 4 ),
 ( 5.733388419619902088, 5.983100554402347449 ),
 .UNSPECIFIED. ) 
 CURVE ( )  GEOMETRIC_REPRESENTATION_ITEM ( )  RATIONAL_B_SPLINE_CURVE ( ( 1.000000000000000000, 0.9948104011409417691, 0.9948104011409417691, 1.000000000000000000 ) ) 
 REPRESENTATION_ITEM ( '' )  );
#3002=ORIENTED_EDGE ( 'NONE', *, *, #22460, .F. ) ;
#3007=ORIENTED_EDGE ( 'NONE', *, *, #246684, .F. ) ;
#3116=ORIENTED_EDGE ( 'NONE', *, *, #57374, .F. ) ;
#3354=CLOSED_SHELL ( 'NONE', ( #66761, #19567, #56713, #119115, #153453, #98265, #119086, #56516, #199323, #173094, #32378, #148677, #104582, #13184, #39626, #190476, #190951, #51676, #28817, #105007, #190046, #7462, #168773, #199139, #152618, #215761, #161559, #162438, #2201, #161248, #150199, #215913, #121562, #154167, #34032, #217275, #52897, #158738, #15752, #213383, #126531, #151268, #90680, #212783, #203830, #66859, #180074, #64338, #19005, #95564, #257720, #120766, #138913 ) ) ;
#3425=VECTOR ( 'NONE', #198220, 1000.000000000000000 ) ;
#3430=EDGE_CURVE ( 'NONE', #238447, #230022, #43469, .T. ) ;
#3437=EDGE_CURVE ( 'NONE', #62835, #152894, #43667, .T. ) ;
#3531=AXIS2_PLACEMENT_3D ( 'NONE', #90822, #13875, #93397 ) ;
#3667=VERTEX_POINT ( 'NONE', #221482 ) ;
#3670=VECTOR ( 'NONE', #42801, 1000.000000000000000 ) ;
#3729=CARTESIAN_POINT ( 'NONE',  ( -16.92925196614875460, 66.02766820360217537, -157.4063626368076143 ) ) ;
#3850=VECTOR ( 'NONE', #190444, 1000.000000000000000 ) ;
#4012=CARTESIAN_POINT ( 'NONE',  ( 18.39999999999999503, 64.25000000001230660, -157.3731074845244393 ) ) ;
#4065=DIRECTION ( 'NONE',  ( -1.000000000000000000, -1.652117596168391700E-15, -1.153667551319263085E-29 ) ) ;
#4073=AXIS2_PLACEMENT_3D ( 'NONE', #251745, #73144, #232206 ) ;
#4097=EDGE_CURVE ( 'NONE', #224786, #244466, #201310, .T. ) ;
#4168=ORIENTED_EDGE ( 'NONE', *, *, #29647, .F. ) ;
#4549=CARTESIAN_POINT ( 'NONE',  ( -16.93344882324368683, 66.00341123272436050, -149.1100817897194872 ) ) ;
#4697=VERTEX_POINT ( 'NONE', #39409 ) ;
#4701=EDGE_LOOP ( 'NONE', ( #5823, #16617, #150156, #163158, #256925, #53521 ) ) ;
#4880=CARTESIAN_POINT ( 'NONE',  ( -23.25000000000000355, 65.95000000001225260, -149.2731074845244450 ) ) ;
#4958=AXIS2_PLACEMENT_3D ( 'NONE', #62286, #6145, #25730 ) ;
#5448=CARTESIAN_POINT ( 'NONE',  ( -16.80100426158792004, 66.05684947961613318, -157.3401617316904151 ) ) ;
#5623=CARTESIAN_POINT ( 'NONE',  ( -16.94062896051973865, 66.00728089491161654, -157.4205909424056244 ) ) ;
#5823=ORIENTED_EDGE ( 'NONE', *, *, #102453, .T. ) ;
#6078=VERTEX_POINT ( 'NONE', #203174 ) ;
#6145=DIRECTION ( 'NONE',  ( 1.186688945009009831E-16, 1.000000000000000000, 6.982962677686266711E-15 ) ) ;
#6176=CARTESIAN_POINT ( 'NONE',  ( -15.15766958671844300, 66.58946139148341103, -154.5904194873835422 ) ) ;
#6358=EDGE_CURVE ( 'NONE', #84754, #3667, #18142, .T. ) ;
#6422=CARTESIAN_POINT ( 'NONE',  ( 18.39999999999999147, 67.17743825834591576, -160.7731074845244166 ) ) ;
#6481=ORIENTED_EDGE ( 'NONE', *, *, #210862, .F. ) ;
#6785=CARTESIAN_POINT ( 'NONE',  ( 23.24999999999999645, 67.17743825834583049, -149.1731074845244223 ) ) ;
#6975=DIRECTION ( 'NONE',  ( 0.2834754621636358940, 0.2834754621636501049, -0.9161240771326873977 ) ) ;
#7391=CARTESIAN_POINT ( 'NONE',  ( -16.83558968593882454, 66.05000000001230376, -157.3608022969076785 ) ) ;
#7462=ADVANCED_FACE ( 'NONE', ( #65316 ), #200985, .T. ) ;
#7524=ORIENTED_EDGE ( 'NONE', *, *, #209466, .F. ) ;
#7530=CARTESIAN_POINT ( 'NONE',  ( -16.88005004766534967, 66.04989949669119653, -149.1727713725756530 ) ) ;
#7580=PLANE ( 'NONE',  #223471 ) ;
#7694=CARTESIAN_POINT ( 'NONE',  ( 13.99999999999999822, 66.15000000001228386, -153.2731074845244450 ) ) ;
#7813=VECTOR ( 'NONE', #27399, 1000.000000000000000 ) ;
#7895=EDGE_CURVE ( 'NONE', #133198, #84754, #48009, .T. ) ;
#8391=EDGE_CURVE ( 'NONE', #152894, #220255, #175391, .T. ) ;
#8761=CARTESIAN_POINT ( 'NONE',  ( -13.43673303185030399, 66.55335100938341952, -154.9339441886012310 ) ) ;
#8806=AXIS2_PLACEMENT_3D ( 'NONE', #186390, #127694, #207236 ) ;
#9098=ORIENTED_EDGE ( 'NONE', *, *, #180528, .T. ) ;
#9318=CARTESIAN_POINT ( 'NONE',  ( 12.42718393586867087, 66.62934494888880010, -152.4972842285435490 ) ) ;
#9370=DIRECTION ( 'NONE',  ( 1.073024830501117725E-15, 6.982962677686266711E-15, -1.000000000000000000 ) ) ;
#9499=CARTESIAN_POINT ( 'NONE',  ( -17.11825945287482753, 66.05000000001230376, -157.2731074845244166 ) ) ;
#9536=CARTESIAN_POINT ( 'NONE',  ( -18.40000000000000213, 64.52683809664974035, -149.0731074845244279 ) ) ;
#9548=ORIENTED_EDGE ( 'NONE', *, *, #230996, .T. ) ;
#9927=VECTOR ( 'NONE', #220425, 1000.000000000000000 ) ;
#9970=CARTESIAN_POINT ( 'NONE',  ( -16.84793658983426923, 66.05000000001230376, -157.2894608067144304 ) ) ;
#10216=SHAPE_REPRESENTATION ( 'Snap Open Cable Crossbars 12', ( #2425 ), #127326 ) ;
#10332=CARTESIAN_POINT ( 'NONE',  ( -18.40000000000000213, 64.66825945288707089, -149.1731074845244507 ) ) ;
#10537=( BOUNDED_SURFACE ( )  B_SPLINE_SURFACE ( 3, 2, ( 
 ( #56585, #158328, #116599 ),
 ( #196136, #17489, #137425 ),
 ( #237829, #96990, #179170 ),
 ( #176593, #256046, #198699 ) ),
 .UNSPECIFIED., .F., .F., .F. ) 
 B_SPLINE_SURFACE_WITH_KNOTS ( ( 4, 4 ),
 ( 3, 3 ),
 ( 0.0008258556059633759532, 0.0009616864997632702718 ),
 ( 0.000000000000000000, 1.000000000000000000 ),
 .UNSPECIFIED. ) 
 GEOMETRIC_REPRESENTATION_ITEM ( )  RATIONAL_B_SPLINE_SURFACE ( (
 ( 1.000000000000000000, 0.9152888060719485130, 1.000000000000000000),
 ( 1.000000000000000000, 0.9327727094138529296, 1.000000000000000000),
 ( 1.000000000000000000, 0.9369023509257985438, 1.000000000000000000),
 ( 1.000000000000000000, 0.9246339933864583527, 1.000000000000000000) ) ) 
 REPRESENTATION_ITEM ( '' )  SURFACE ( )  );
#10567=DIRECTION ( 'NONE',  ( -0.000000000000000000, -6.982962677686266711E-15, 1.000000000000000000 ) ) ;
#10604=CARTESIAN_POINT ( 'NONE',  ( -16.92280123533733871, 66.05000000001224691, -149.3737397986104725 ) ) ;
#10756=CARTESIAN_POINT ( 'NONE',  ( -16.87851181299898684, 66.04995707600456001, -157.3732509998913258 ) ) ;
#10813=COLOUR_RGB ( '', 0.72549020, 0.75294118, 0.79215686) ;
#10940=CIRCLE ( 'NONE', #44255, 0.09999999999999939493 ) ;
#11081=EDGE_CURVE ( 'NONE', #80528, #16882, #191457, .T. ) ;
#11148=DIRECTION ( 'NONE',  ( -1.020425574104004196E-15, -6.982962677686266711E-15, 1.000000000000000000 ) ) ;
#11307=FACE_OUTER_BOUND ( 'NONE', #229209, .T. ) ;
#11430=ORIENTED_EDGE ( 'NONE', *, *, #60269, .F. ) ;
#11498=CARTESIAN_POINT ( 'NONE',  ( -16.97092634996621641, 65.99911103366444820, -157.3929647182265228 ) ) ;
#11604=DIRECTION ( 'NONE',  ( 1.000000000000000000, 0.000000000000000000, 0.000000000000000000 ) ) ;
#11627=EDGE_CURVE ( 'NONE', #14807, #4697, #42936, .T. ) ;
#11769=ORIENTED_EDGE ( 'NONE', *, *, #68276, .F. ) ;
#11832=DIRECTION ( 'NONE',  ( -0.000000000000000000, -6.982962677686266711E-15, 1.000000000000000000 ) ) ;
#11838=EDGE_LOOP ( 'NONE', ( #238963, #7524, #256693, #75065, #254393, #132251, #133087, #131625, #219176, #231638, #73102, #181645, #248350, #18936 ) ) ;
#11915=CARTESIAN_POINT ( 'NONE',  ( 15.07585980824112326, 66.58236703690597835, -151.8741590187921986 ) ) ;
#11935=DIRECTION ( 'NONE',  ( 0.000000000000000000, -1.000000000000000000, -6.982962677686266711E-15 ) ) ;
#12080=EDGE_CURVE ( 'NONE', #53606, #250417, #164761, .T. ) ;
#12489=( NAMED_UNIT ( * ) PLANE_ANGLE_UNIT ( ) SI_UNIT ( $, .RADIAN. ) );
#12495=VECTOR ( 'NONE', #154214, 1000.000000000000000 ) ;
#12693=CARTESIAN_POINT ( 'NONE',  ( -16.88328101497759448, 66.04964716579338813, -149.1719279695951457 ) ) ;
#12701=DIRECTION ( 'NONE',  ( 0.000000000000000000, 6.982962677686266711E-15, -1.000000000000000000 ) ) ;
#12742=AXIS2_PLACEMENT_3D ( 'NONE', #178880, #84834, #125293 ) ;
#12802=CARTESIAN_POINT ( 'NONE',  ( -16.91049119928362643, 66.05000000001223270, -149.1413870913335415 ) ) ;
#12899=DIRECTION ( 'NONE',  ( -0.000000000000000000, -6.982962677686266711E-15, 1.000000000000000000 ) ) ;
#12909=ORIENTED_EDGE ( 'NONE', *, *, #142449, .F. ) ;
#13146=LINE ( 'NONE', #153981, #101631 ) ;
#13184=ADVANCED_FACE ( 'NONE', ( #222555 ), #178347, .F. ) ;
#13430=VERTEX_POINT ( 'NONE', #54200 ) ;
#13498=ORIENTED_EDGE ( 'NONE', *, *, #65681, .F. ) ;
#13612=DIRECTION ( 'NONE',  ( 0.000000000000000000, -6.982962677686266711E-15, 1.000000000000000000 ) ) ;
#13708=CARTESIAN_POINT ( 'NONE',  ( -18.40000000000000213, 70.35000000001230092, -157.3731074845244109 ) ) ;
#13719=CARTESIAN_POINT ( 'NONE',  ( 17.74533788810831325, 65.18150020854152160, -159.7094848095768498 ) ) ;
#13809=EDGE_CURVE ( 'NONE', #124544, #167594, #34052, .T. ) ;
#13875=DIRECTION ( 'NONE',  ( 0.000000000000000000, 1.000000000000000000, 6.982962677686266711E-15 ) ) ;
#13913=VECTOR ( 'NONE', #11832, 1000.000000000000000 ) ;
#14212=DIRECTION ( 'NONE',  ( -1.000000000000000000, 0.000000000000000000, -0.000000000000000000 ) ) ;
#14451=LINE ( 'NONE', #254295, #164794 ) ;
#14485=CARTESIAN_POINT ( 'NONE',  ( 14.22916352759893499, 66.54258906972209786, -151.5231915757781849 ) ) ;
#14620=CARTESIAN_POINT ( 'NONE',  ( -21.64999999999999858, 65.95000000001232365, -157.3731074845244393 ) ) ;
#14807=VERTEX_POINT ( 'NONE', #109720 ) ;
#14842=CARTESIAN_POINT ( 'NONE',  ( -16.77683809663752257, 66.05416425680813575, -157.3591584654202222 ) ) ;
#15017=PLANE ( 'NONE',  #55231 ) ;
#15172=VECTOR ( 'NONE', #94721, 1000.000000000000000 ) ;
#15476=ORIENTED_EDGE ( 'NONE', *, *, #23308, .T. ) ;
#15516=CARTESIAN_POINT ( 'NONE',  ( -16.86578989773641624, 66.01519019875350125, -157.4877723711466615 ) ) ;
#15752=ADVANCED_FACE ( 'NONE', ( #75157 ), #98491, .T. ) ;
#15884=LINE ( 'NONE', #249661, #218526 ) ;
#15911=FACE_OUTER_BOUND ( 'NONE', #240915, .T. ) ;
#16531=DIRECTION ( 'NONE',  ( 1.000000000000000000, 0.000000000000000000, 0.000000000000000000 ) ) ;
#16617=ORIENTED_EDGE ( 'NONE', *, *, #81161, .T. ) ;
#16768=ORIENTED_EDGE ( 'NONE', *, *, #166442, .T. ) ;
#16841=LINE ( 'NONE', #136755, #108716 ) ;
#16882=VERTEX_POINT ( 'NONE', #162430 ) ;
#17031=CARTESIAN_POINT ( 'NONE',  ( 17.23472005113827166, 65.69211804551146372, -147.9765306244557621 ) ) ;
#17214=DIRECTION ( 'NONE',  ( 1.000000000000000000, -0.000000000000000000, 0.000000000000000000 ) ) ;
#17337=ORIENTED_EDGE ( 'NONE', *, *, #54937, .F. ) ;
#17339=VERTEX_POINT ( 'NONE', #225923 ) ;
#17489=CARTESIAN_POINT ( 'NONE',  ( -16.89797118371616591, 66.02361927736852465, -157.4604008520840921 ) ) ;
#17502=CARTESIAN_POINT ( 'NONE',  ( 18.54999999999999716, 67.25000000001222134, -149.1731074845244223 ) ) ;
#17893=CARTESIAN_POINT ( 'NONE',  ( -17.11825945287481687, 66.05000000001224691, -149.2731074845244450 ) ) ;
#17926=LINE ( 'NONE', #158761, #232483 ) ;
#17950=ORIENTED_EDGE ( 'NONE', *, *, #222939, .T. ) ;
#18049=ORIENTED_EDGE ( 'NONE', *, *, #142107, .T. ) ;
#18142=LINE ( 'NONE', #254170, #185671 ) ;
#18265=VERTEX_POINT ( 'NONE', #118238 ) ;
#18311=DIRECTION ( 'NONE',  ( -0.7071067811865487940, -0.7071067811865463515, -4.216150419019404490E-15 ) ) ;
#18925=VERTEX_POINT ( 'NONE', #122456 ) ;
#18936=ORIENTED_EDGE ( 'NONE', *, *, #232710, .T. ) ;
#18944=DIRECTION ( 'NONE',  ( -1.652117596168391700E-15, 1.000000000000000000, 6.982962677686266711E-15 ) ) ;
#19005=ADVANCED_FACE ( 'NONE', ( #227964 ), #101990, .T. ) ;
#19138=CARTESIAN_POINT ( 'NONE',  ( 15.48841904831874849, 67.43841904833107037, -157.3731074845244393 ) ) ;
#19565=DIRECTION ( 'NONE',  ( -0.000000000000000000, -6.982962677686266711E-15, 1.000000000000000000 ) ) ;
#19567=ADVANCED_FACE ( 'NONE', ( #95812 ), #211950, .F. ) ;
#19763=CARTESIAN_POINT ( 'NONE',  ( -16.78493211734303614, 66.05416425680807890, -149.1870565036285257 ) ) ;
#19912=ORIENTED_EDGE ( 'NONE', *, *, #235281, .F. ) ;
#20134=CARTESIAN_POINT ( 'NONE',  ( -16.81744102076748959, 66.05000000001224691, -149.1731074845244223 ) ) ;
#20643=CARTESIAN_POINT ( 'NONE',  ( -16.86379686415369861, 66.02478224075913715, -157.4564973736146953 ) ) ;
#20884=ORIENTED_EDGE ( 'NONE', *, *, #253906, .T. ) ;
#21178=LINE ( 'NONE', #160690, #969 ) ;
#21238=EDGE_CURVE ( 'NONE', #47244, #252649, #69724, .T. ) ;
#21248=EDGE_LOOP ( 'NONE', ( #172753, #148188 ) ) ;
#21400=CARTESIAN_POINT ( 'NONE',  ( -23.25000000000000355, 70.35000000001224407, -149.1731074845243938 ) ) ;
#21539=CARTESIAN_POINT ( 'NONE',  ( -21.64999999999999858, 66.65000000001234071, -160.7731074845244166 ) ) ;
#21684=CIRCLE ( 'NONE', #229781, 0.09999999999998898659 ) ;
#21704=ORIENTED_EDGE ( 'NONE', *, *, #11627, .F. ) ;
#21853=CARTESIAN_POINT ( 'NONE',  ( -16.91776028072577631, 66.03659960638248094, -149.1480834698222964 ) ) ;
#21949=CARTESIAN_POINT ( 'NONE',  ( 13.99999999999999822, 66.15000000001228386, -153.2731074845244450 ) ) ;
#21982=DIRECTION ( 'NONE',  ( -1.073024830501117725E-15, -6.982962677686266711E-15, 1.000000000000000000 ) ) ;
#21998=CARTESIAN_POINT ( 'NONE',  ( -16.87036670365548474, 66.01058118071060221, -149.0435473672224020 ) ) ;
#22139=LINE ( 'NONE', #162935, #170283 ) ;
#22142=B_SPLINE_CURVE_WITH_KNOTS ( 'NONE', 3,
 ( #81144, #45884, #180270, #5448, #26334, #181569, #105835, #238966, #42056, #84978, #199849, #40787, #220680, #2890 ),
 .UNSPECIFIED., .F., .F.,
 ( 4, 2, 2, 2, 2, 2, 4 ),
 ( 0.000000000000000000, 2.389617747647320093E-05, 4.779235495294640186E-05, 9.558470990581376537E-05, 0.0001911694198115567594, 0.0003823388396230466778, 0.0007646776792461088598 ),
 .UNSPECIFIED. ) ;
#22326=VERTEX_POINT ( 'NONE', #48383 ) ;
#22358=DIRECTION ( 'NONE',  ( -1.000000000000000000, 0.000000000000000000, -0.000000000000000000 ) ) ;
#22384=ORIENTED_EDGE ( 'NONE', *, *, #36961, .F. ) ;
#22460=EDGE_CURVE ( 'NONE', #124544, #222558, #255009, .T. ) ;
#22675=CARTESIAN_POINT ( 'NONE',  ( -16.93772744219066340, 66.00645889125993904, -157.4250455125547035 ) ) ;
#22893=DIRECTION ( 'NONE',  ( 0.000000000000000000, 6.982962677686266711E-15, -1.000000000000000000 ) ) ;
#23067=ORIENTED_EDGE ( 'NONE', *, *, #148070, .T. ) ;
#23142=CARTESIAN_POINT ( 'NONE',  ( -16.88705144915433110, 66.05000000001230376, -157.0921288898123578 ) ) ;
#23308=EDGE_CURVE ( 'NONE', #96826, #215608, #34658, .T. ) ;
#23465=DIRECTION ( 'NONE',  ( -0.5932847527679298016, -0.8049926720990051576, -5.621233785078291429E-15 ) ) ;
#23513=ORIENTED_EDGE ( 'NONE', *, *, #221889, .F. ) ;
#24004=DIRECTION ( 'NONE',  ( 1.000000000000000000, 7.492892343619937423E-30, -1.073024830501117725E-15 ) ) ;
#24042=CARTESIAN_POINT ( 'NONE',  ( -13.54036565897074240, 66.54845833862674453, -151.5692319856938184 ) ) ;
#24178=ORIENTED_EDGE ( 'NONE', *, *, #81161, .F. ) ;
#24206=ORIENTED_EDGE ( 'NONE', *, *, #213297, .T. ) ;
#24327=LINE ( 'NONE', #183389, #191695 ) ;
#24428=CARTESIAN_POINT ( 'NONE',  ( -16.96982749440685012, 66.05000000001230376, -156.8983290757135194 ) ) ;
#24485=CARTESIAN_POINT ( 'NONE',  ( -17.29158576265543346, 65.63525233399438719, -158.6058657293166050 ) ) ;
#24487=FACE_OUTER_BOUND ( 'NONE', #49530, .T. ) ;
#24680=( NAMED_UNIT ( * ) SI_UNIT ( $, .STERADIAN. ) SOLID_ANGLE_UNIT ( ) );
#24761=VERTEX_POINT ( 'NONE', #105219 ) ;
#24865=VERTEX_POINT ( 'NONE', #109106 ) ;
#25046=EDGE_CURVE ( 'NONE', #67597, #196307, #101050, .T. ) ;
#25079=LINE ( 'NONE', #66751, #206069 ) ;
#25080=( BOUNDED_SURFACE ( )  B_SPLINE_SURFACE ( 3, 2, ( 
 ( #155245, #153977, #35304 ),
 ( #194365, #254287, #234745 ),
 ( #56080, #135632, #156532 ),
 ( #236023, #1245, #83338 ) ),
 .UNSPECIFIED., .F., .F., .F. ) 
 B_SPLINE_SURFACE_WITH_KNOTS ( ( 4, 4 ),
 ( 3, 3 ),
 ( 0.3000847527772363410, 0.5552748953338753068 ),
 ( 0.000000000000000000, 1.000000000000000000 ),
 .UNSPECIFIED. ) 
 GEOMETRIC_REPRESENTATION_ITEM ( )  RATIONAL_B_SPLINE_SURFACE ( (
 ( 1.000000000000000000, 0.9152888060719485130, 1.000000000000000000),
 ( 1.000000000000000000, 0.9104333467450272943, 1.000000000000000000),
 ( 1.000000000000000000, 0.9035312726220733337, 1.000000000000000000),
 ( 1.000000000000000000, 0.8946697475932141597, 1.000000000000000000) ) ) 
 REPRESENTATION_ITEM ( '' )  SURFACE ( )  );
#25200=CARTESIAN_POINT ( 'NONE',  ( -16.80939487329395021, 66.05000000001224691, -149.1731074845235696 ) ) ;
#25229=CARTESIAN_POINT ( 'NONE',  ( -16.92989143108097849, 66.05000000001230376, -157.1406236097677152 ) ) ;
#25236=CARTESIAN_POINT ( 'NONE',  ( -16.93226657140833069, 66.00045617728787306, -157.4443943735508071 ) ) ;
#25329=CARTESIAN_POINT ( 'NONE',  ( -15.39126916658603150, 66.61042836546582180, -152.2054667721552050 ) ) ;
#25426=CARTESIAN_POINT ( 'NONE',  ( -16.93294127766158752, 65.99671989705738895, -149.0932002186951877 ) ) ;
#25477=EDGE_CURVE ( 'NONE', #84754, #114211, #243239, .T. ) ;
#25730=DIRECTION ( 'NONE',  ( 1.000000000000000000, -1.186688945009009831E-16, -8.286604613020806758E-31 ) ) ;
#25754=CARTESIAN_POINT ( 'NONE',  ( -15.52965525596988527, 66.62446189796426665, -154.1532316035335555 ) ) ;
#25877=EDGE_LOOP ( 'NONE', ( #109433, #108807, #125141, #200957 ) ) ;
#25957=ORIENTED_EDGE ( 'NONE', *, *, #216098, .T. ) ;
#25986=EDGE_CURVE ( 'NONE', #6078, #191026, #144895, .T. ) ;
#26318=ADVANCED_BREP_SHAPE_REPRESENTATION ( '', ( #194237, #2425 ), #127326 ) ;
#26334=CARTESIAN_POINT ( 'NONE',  ( -16.80468759584937644, 66.05784632487818442, -157.3330886183227904 ) ) ;
#26401=ORIENTED_EDGE ( 'NONE', *, *, #157424, .F. ) ;
#26510=CARTESIAN_POINT ( 'NONE',  ( -16.89020380669786192, 66.05000000001230376, -157.2656963364138676 ) ) ;
#26632=EDGE_CURVE ( 'NONE', #18265, #68090, #139846, .T. ) ;
#26689=DIRECTION ( 'NONE',  ( 1.000000000000000000, 0.000000000000000000, 0.000000000000000000 ) ) ;
#27013=CARTESIAN_POINT ( 'NONE',  ( -14.00000000000000178, 66.15000000001228386, -153.2731074845244166 ) ) ;
#27172=DIRECTION ( 'NONE',  ( 0.000000000000000000, -6.982962677686266711E-15, 1.000000000000000000 ) ) ;
#27230=CARTESIAN_POINT ( 'NONE',  ( -17.11825945287482753, 65.95000000001232365, -157.3731074845244109 ) ) ;
#27232=ORIENTED_EDGE ( 'NONE', *, *, #13809, .T. ) ;
#27399=DIRECTION ( 'NONE',  ( 0.000000000000000000, -1.000000000000000000, -6.982962677686266711E-15 ) ) ;
#27451=CARTESIAN_POINT ( 'NONE',  ( -16.87036670365548474, 66.01058118071058800, -149.0435473672224020 ) ) ;
#27545=EDGE_CURVE ( 'NONE', #67174, #59001, #215000, .T. ) ;
#27659=CARTESIAN_POINT ( 'NONE',  ( -17.29158576265543346, 65.63525233399431613, -147.9403492397322566 ) ) ;
#27756=ORIENTED_EDGE ( 'NONE', *, *, #23308, .F. ) ;
#28131=EDGE_CURVE ( 'NONE', #59001, #158817, #233832, .T. ) ;
#28639=DIRECTION ( 'NONE',  ( -1.000000000000000000, 0.000000000000000000, 0.000000000000000000 ) ) ;
#28817=ADVANCED_FACE ( 'NONE', ( #237999 ), #59333, .F. ) ;
#28936=CARTESIAN_POINT ( 'NONE',  ( 15.39170923737818342, 66.61047060254553287, -152.2059995716307128 ) ) ;
#28975=CARTESIAN_POINT ( 'NONE',  ( 20.04999999999999716, 67.25000000001227818, -157.3731074845244109 ) ) ;
#29110=CARTESIAN_POINT ( 'NONE',  ( 20.99999999999999645, 66.25000000001226397, -149.1731074845244223 ) ) ;
#29336=PRODUCT_DEFINITION ( 'UNKNOWN', '', #115392, #134062 ) ;
#29432=LINE ( 'NONE', #232745, #235868 ) ;
#29568=CARTESIAN_POINT ( 'NONE',  ( -16.88783316861828609, 66.05000000001230376, -157.2708434425446455 ) ) ;
#29581=ORIENTED_EDGE ( 'NONE', *, *, #7895, .T. ) ;
#29647=EDGE_CURVE ( 'NONE', #17339, #132836, #143435, .T. ) ;
#30000=ORIENTED_EDGE ( 'NONE', *, *, #96157, .F. ) ;
#30014=EDGE_CURVE ( 'NONE', #232094, #152894, #118444, .T. ) ;
#30114=ORIENTED_EDGE ( 'NONE', *, *, #242400, .T. ) ;
#30288=ORIENTED_EDGE ( 'NONE', *, *, #157523, .T. ) ;
#30381=EDGE_CURVE ( 'NONE', #128197, #158817, #142787, .T. ) ;
#30662=VECTOR ( 'NONE', #46004, 1000.000000000000000 ) ;
#30671=ORIENTED_EDGE ( 'NONE', *, *, #115796, .F. ) ;
#30705=DIRECTION ( 'NONE',  ( 0.000000000000000000, -6.982962677686266711E-15, 1.000000000000000000 ) ) ;
#31135=DIRECTION ( 'NONE',  ( 1.000000000000000000, 0.000000000000000000, 0.000000000000000000 ) ) ;
#31224=EDGE_CURVE ( 'NONE', #225539, #232013, #14451, .T. ) ;
#31275=DIRECTION ( 'NONE',  ( -1.000000000000000000, 0.000000000000000000, 0.000000000000000000 ) ) ;
#31486=CARTESIAN_POINT ( 'NONE',  ( 12.30626653967341788, 66.64320997496639620, -152.8182809759105112 ) ) ;
#32028=CARTESIAN_POINT ( 'NONE',  ( 17.23472005113828232, 65.69211804551153477, -158.5696843445931279 ) ) ;
#32043=EDGE_CURVE ( 'NONE', #201378, #42338, #22142, .T. ) ;
#32044=DIRECTION ( 'NONE',  ( 1.186688945009010077E-16, 1.000000000000000000, 6.982962677686266711E-15 ) ) ;
#32095=CARTESIAN_POINT ( 'NONE',  ( -16.87331047859651179, 66.05000000001230376, -157.3731074845244393 ) ) ;
#32253=CARTESIAN_POINT ( 'NONE',  ( -16.87665923198281348, 66.05000000001224691, -149.1731074845244223 ) ) ;
#32267=ORIENTED_EDGE ( 'NONE', *, *, #172856, .T. ) ;
#32378=ADVANCED_FACE ( 'NONE', ( #236073 ), #136971, .F. ) ;
#32558=VERTEX_POINT ( 'NONE', #245060 ) ;
#32674=DIRECTION ( 'NONE',  ( -1.000000000000000000, -1.652117596168391700E-15, -1.153667551319263085E-29 ) ) ;
#32777=CARTESIAN_POINT ( 'NONE',  ( 15.74999999999999645, 66.65000000001228386, -153.2731074845244166 ) ) ;
#32842=CARTESIAN_POINT ( 'NONE',  ( -16.77683809663752257, 52.34166666667894674, -153.2731074845245303 ) ) ;
#32986=AXIS2_PLACEMENT_3D ( 'NONE', #173224, #212315, #140115 ) ;
#33165=ORIENTED_EDGE ( 'NONE', *, *, #157157, .F. ) ;
#33498=CARTESIAN_POINT ( 'NONE',  ( -13.77178122865955068, 66.54397173950437150, -155.0119094494586989 ) ) ;
#33568=DIRECTION ( 'NONE',  ( 1.000000000000000000, 0.000000000000000000, 0.000000000000000000 ) ) ;
#33571=CARTESIAN_POINT ( 'NONE',  ( -18.34374000495060386, 64.52683809664983983, -160.7731074845244450 ) ) ;
#33709=CARTESIAN_POINT ( 'NONE',  ( 20.09999999999999787, 66.25000000001233502, -160.7731074845244166 ) ) ;
#33722=LINE ( 'NONE', #91080, #116674 ) ;
#33731=ORIENTED_EDGE ( 'NONE', *, *, #166442, .F. ) ;
#33961=DIRECTION ( 'NONE',  ( 0.000000000000000000, 1.000000000000000000, 0.000000000000000000 ) ) ;
#34032=ADVANCED_FACE ( 'NONE', ( #24487 ), #79278, .F. ) ;
#34052=LINE ( 'NONE', #251775, #180841 ) ;
#34058=CARTESIAN_POINT ( 'NONE',  ( 13.43663047529820176, 66.55335465531702255, -151.6123010284242412 ) ) ;
#34144=EDGE_CURVE ( 'NONE', #257702, #257588, #178180, .T. ) ;
#34205=CARTESIAN_POINT ( 'NONE',  ( -16.87683809663752044, 66.13508655273203374, -149.7988259332204279 ) ) ;
#34320=LINE ( 'NONE', #254594, #42774 ) ;
#34342=CARTESIAN_POINT ( 'NONE',  ( -21.64999999999999858, 66.65000000001231228, -157.3731074845244393 ) ) ;
#34587=CARTESIAN_POINT ( 'NONE',  ( -17.73285935862574902, 65.14201819622893197, -159.7816692942933230 ) ) ;
#34658=LINE ( 'NONE', #195013, #241605 ) ;
#34741=DIRECTION ( 'NONE',  ( 0.000000000000000000, 1.000000000000000000, 6.982962677686266711E-15 ) ) ;
#34791=CARTESIAN_POINT ( 'NONE',  ( -23.25000000000000355, 64.25000000001233502, -160.7731074845244450 ) ) ;
#34985=CARTESIAN_POINT ( 'NONE',  ( 20.05000000000002913, 68.75000000001227818, -157.3731074845244109 ) ) ;
#35045=ORIENTED_EDGE ( 'NONE', *, *, #151671, .T. ) ;
#35304=CARTESIAN_POINT ( 'NONE',  ( -16.87036670365547408, 66.01058118071060221, -149.0435473672224305 ) ) ;
#35335=CARTESIAN_POINT ( 'NONE',  ( -16.84981964351528916, 66.08268176591339227, -149.3927090985447705 ) ) ;
#35388=CARTESIAN_POINT ( 'NONE',  ( -18.38817693311004575, 64.51850848411244499, -145.7731074845244450 ) ) ;
#35515=DIRECTION ( 'NONE',  ( 0.000000000000000000, -1.000000000000000000, -6.982962677686266711E-15 ) ) ;
#35626=VECTOR ( 'NONE', #62222, 1000.000000000000000 ) ;
#35765=VECTOR ( 'NONE', #43891, 1000.000000000000000 ) ;
#35835=SURFACE_STYLE_USAGE ( .BOTH. , #136162 ) ;
#36613=CARTESIAN_POINT ( 'NONE',  ( -16.80891096016306108, 66.05000000001224691, -149.1554446772547635 ) ) ;
#36633=CARTESIAN_POINT ( 'NONE',  ( -16.97683809663752186, 66.05000000001226113, -149.9254715027207681 ) ) ;
#36662=CARTESIAN_POINT ( 'NONE',  ( 13.12220780326570768, 66.56936653093944756, -154.7913416897003174 ) ) ;
#36961=EDGE_CURVE ( 'NONE', #158817, #215723, #74851, .T. ) ;
#37005=ORIENTED_EDGE ( 'NONE', *, *, #142107, .F. ) ;
#37231=ORIENTED_EDGE ( 'NONE', *, *, #31224, .T. ) ;
#37938=CARTESIAN_POINT ( 'NONE',  ( -18.38204789744325396, 64.52049896284712815, -145.7731074845244450 ) ) ;
#38025=CYLINDRICAL_SURFACE ( 'NONE', #169209, 1.500000000000001332 ) ;
#38080=ORIENTED_EDGE ( 'NONE', *, *, #207080, .T. ) ;
#38137=CARTESIAN_POINT ( 'NONE',  ( 22.88900146558018989, 67.29609520889943042, -149.1731074845244223 ) ) ;
#38394=CARTESIAN_POINT ( 'NONE',  ( 23.24999999999999645, 67.17743825834591576, -160.7731074845244166 ) ) ;
#38436=CARTESIAN_POINT ( 'NONE',  ( 23.04999999999999716, 67.17743825834583049, -149.1731074845244223 ) ) ;
#38445=CARTESIAN_POINT ( 'NONE',  ( -12.30589683808040924, 66.64325398293399871, -152.8197477631601657 ) ) ;
#38526=DIRECTION ( 'NONE',  ( -1.000000000000000000, -1.652117596168391700E-15, -1.153667551319263085E-29 ) ) ;
#38603=DIRECTION ( 'NONE',  ( -1.000000000000000000, 0.000000000000000000, 0.000000000000000000 ) ) ;
#38970=DIRECTION ( 'NONE',  ( 0.000000000000000000, -1.000000000000000000, -6.982962677686266711E-15 ) ) ;
#38980=PLANE ( 'NONE',  #102914 ) ;
#39124=FACE_OUTER_BOUND ( 'NONE', #69189, .T. ) ;
#39376=VECTOR ( 'NONE', #140546, 1000.000000000000000 ) ;
#39409=CARTESIAN_POINT ( 'NONE',  ( 18.39999999999997371, 64.52683809664972614, -145.7731074845244450 ) ) ;
#39491=ORIENTED_EDGE ( 'NONE', *, *, #117642, .F. ) ;
#39626=ADVANCED_FACE ( 'NONE', ( #46790 ), #147189, .F. ) ;
#39686=ORIENTED_EDGE ( 'NONE', *, *, #29647, .T. ) ;
#39893=AXIS2_PLACEMENT_3D ( 'NONE', #196941, #18311, #97817 ) ;
#39896=VECTOR ( 'NONE', #253181, 1000.000000000000000 ) ;
#40525=CARTESIAN_POINT ( 'NONE',  ( -18.36973785203556275, 64.52449679952799499, -145.7731074845244450 ) ) ;
#40787=CARTESIAN_POINT ( 'NONE',  ( -16.87372386987899020, 66.11939976637552263, -156.8738376126579794 ) ) ;
#40875=DIRECTION ( 'NONE',  ( 1.000000000000000000, 0.000000000000000000, 0.000000000000000000 ) ) ;
#40977=ORIENTED_EDGE ( 'NONE', *, *, #52301, .T. ) ;
#41150=CARTESIAN_POINT ( 'NONE',  ( -16.93415306273742260, 66.00437773999972535, -149.1130505421640180 ) ) ;
#41223=DIRECTION ( 'NONE',  ( 0.000000000000000000, -1.000000000000000000, -7.813886390323680189E-15 ) ) ;
#41863=ORIENTED_EDGE ( 'NONE', *, *, #85161, .T. ) ;
#42024=ORIENTED_EDGE ( 'NONE', *, *, #172856, .F. ) ;
#42056=CARTESIAN_POINT ( 'NONE',  ( -16.83794237512073266, 66.07364077890480303, -157.2195653258254424 ) ) ;
#42222=CARTESIAN_POINT ( 'NONE',  ( -16.93909480342659890, 66.00692163521075884, -157.4227604678520720 ) ) ;
#42297=ORIENTED_EDGE ( 'NONE', *, *, #195, .T. ) ;
#42302=CARTESIAN_POINT ( 'NONE',  ( -13.77083647240105257, 66.54258906972208365, -151.5231915757781564 ) ) ;
#42338=VERTEX_POINT ( 'NONE', #174056 ) ;
#42774=VECTOR ( 'NONE', #77254, 1000.000000000000000 ) ;
#42801=DIRECTION ( 'NONE',  ( 0.7071067811865463515, 0.7071067811865487940, 4.937700262164540154E-15 ) ) ;
#42845=EDGE_LOOP ( 'NONE', ( #256675, #33731, #256195, #53328, #112366, #132750, #212571, #149961, #256215, #37005, #27756, #30000 ) ) ;
#42848=DIRECTION ( 'NONE',  ( -1.000000000000000000, 0.000000000000000000, 0.000000000000000000 ) ) ;
#42936=LINE ( 'NONE', #200726, #97045 ) ;
#43002=PLANE ( 'NONE',  #83337 ) ;
#43041=ORIENTED_EDGE ( 'NONE', *, *, #246036, .T. ) ;
#43198=ORIENTED_EDGE ( 'NONE', *, *, #242275, .F. ) ;
#43469=B_SPLINE_CURVE_WITH_KNOTS ( 'NONE', 3,
 ( #124316, #63038, #128169, #123034, #25229, #66900, #26510, #65612, #164726, #205107 ),
 .UNSPECIFIED., .F., .F.,
 ( 4, 2, 2, 2, 4 ),
 ( 0.000000000000000000, 0.0003916577441626797819, 0.0005874866162440189410, 0.0006854010522846886019, 0.0007833154883253581544 ),
 .UNSPECIFIED. ) ;
#43504=CARTESIAN_POINT ( 'NONE',  ( -16.93583594267724379, 65.99137656496009186, -157.4637166452036752 ) ) ;
#43554=ORIENTED_EDGE ( 'NONE', *, *, #21238, .T. ) ;
#43588=CARTESIAN_POINT ( 'NONE',  ( -14.11361717019514472, 66.54257354752336084, -151.5230656161243985 ) ) ;
#43667=CIRCLE ( 'NONE', #227004, 0.9000000000000014655 ) ;
#43710=AXIS2_PLACEMENT_3D ( 'NONE', #256807, #157816, #52227 ) ;
#43891=DIRECTION ( 'NONE',  ( -0.000000000000000000, -6.982962677686266711E-15, 1.000000000000000000 ) ) ;
#44252=CARTESIAN_POINT ( 'NONE',  ( -20.65000000000000568, 70.35000000001232934, -160.7731074845243882 ) ) ;
#44255=AXIS2_PLACEMENT_3D ( 'NONE', #244891, #27172, #42848 ) ;
#44394=CARTESIAN_POINT ( 'NONE',  ( -16.27683809663750480, 66.65000000001234071, -160.7731074845244166 ) ) ;
#44540=DIRECTION ( 'NONE',  ( 1.000000000000000000, 7.492892343619937423E-30, -1.073024830501117725E-15 ) ) ;
#44734=EDGE_CURVE ( 'NONE', #172220, #59001, #21684, .T. ) ;
#44752=CARTESIAN_POINT ( 'NONE',  ( -16.77683809663752257, 66.05416425680809311, -149.1870565036286109 ) ) ;
#44980=CARTESIAN_POINT ( 'NONE',  ( -16.93860193097148326, 66.00689223268298633, -149.1229691172175933 ) ) ;
#45027=EDGE_CURVE ( 'NONE', #18265, #210270, #21178, .T. ) ;
#45104=DIRECTION ( 'NONE',  ( 0.000000000000000000, -1.000000000000000000, -7.759275652592821052E-15 ) ) ;
#45140=ORIENTED_EDGE ( 'NONE', *, *, #235445, .T. ) ;
#45246=CARTESIAN_POINT ( 'NONE',  ( -16.93710578446436088, 66.05000000001230376, -157.1043035007245408 ) ) ;
#45420=DIRECTION ( 'NONE',  ( -0.7071067811865487940, -0.7071067811865463515, -4.937700262164522799E-15 ) ) ;
#45446=CARTESIAN_POINT ( 'NONE',  ( -23.25000000000000355, 70.35000000001230092, -157.3731074845244109 ) ) ;
#45660=ORIENTED_EDGE ( 'NONE', *, *, #177478, .F. ) ;
#45683=DIRECTION ( 'NONE',  ( -1.000000000000000000, 0.000000000000000000, 0.000000000000000000 ) ) ;
#45729=EDGE_CURVE ( 'NONE', #220255, #189976, #1362, .T. ) ;
#45801=EDGE_LOOP ( 'NONE', ( #79750, #250906, #20884, #16768 ) ) ;
#45884=CARTESIAN_POINT ( 'NONE',  ( -16.78493832629888516, 66.05416425680813575, -157.3591584654201938 ) ) ;
#45933=VERTEX_POINT ( 'NONE', #125675 ) ;
#45935=EDGE_LOOP ( 'NONE', ( #55934, #131178, #219914, #231411, #184074 ) ) ;
#45937=DIRECTION ( 'NONE',  ( -1.000000000000000000, 4.625929269271478222E-14, 0.000000000000000000 ) ) ;
#46004=DIRECTION ( 'NONE',  ( 0.000000000000000000, -1.000000000000000000, -6.982962677686266711E-15 ) ) ;
#46024=AXIS2_PLACEMENT_3D ( 'NONE', #66268, #67543, #85785 ) ;
#46041=VERTEX_POINT ( 'NONE', #160357 ) ;
#46054=CARTESIAN_POINT ( 'NONE',  ( -16.94107738177415712, 65.98576071487568129, -157.4731074845244336 ) ) ;
#46087=CYLINDRICAL_SURFACE ( 'NONE', #186824, 0.1000000000000050432 ) ;
#46270=ORIENTED_EDGE ( 'NONE', *, *, #102453, .F. ) ;
#46366=LINE ( 'NONE', #125908, #47536 ) ;
#46525=VECTOR ( 'NONE', #17214, 1000.000000000000000 ) ;
#46578=CARTESIAN_POINT ( 'NONE',  ( -14.77738660682464911, 66.56344716000788253, -154.8451520117641280 ) ) ;
#46633=CARTESIAN_POINT ( 'NONE',  ( -16.89208623190940273, 66.04842205103675212, -149.1678352813061394 ) ) ;
#46648=VERTEX_POINT ( 'NONE', #133716 ) ;
#46743=CARTESIAN_POINT ( 'NONE',  ( -17.11825945287482753, 66.05000000001231797, -157.3731074845243825 ) ) ;
#46790=FACE_OUTER_BOUND ( 'NONE', #98395, .T. ) ;
#46878=ORIENTED_EDGE ( 'NONE', *, *, #80827, .T. ) ;
#47064=( BOUNDED_CURVE ( )  B_SPLINE_CURVE ( 3, ( #241397, #1478, #61464, #146128 ),
 .UNSPECIFIED., .F., .F. ) 
 B_SPLINE_CURVE_WITH_KNOTS ( ( 4, 4 ),
 ( 4.712388980384690562, 5.672655318024762749 ),
 .UNSPECIFIED. ) 
 CURVE ( )  GEOMETRIC_REPRESENTATION_ITEM ( )  RATIONAL_B_SPLINE_CURVE ( ( 1.000000000000000000, 0.9246222802177245237, 0.9246222802177245237, 1.000000000000000000 ) ) 
 REPRESENTATION_ITEM ( '' )  );
#47223=VERTEX_POINT ( 'NONE', #98117 ) ;
#47244=VERTEX_POINT ( 'NONE', #78580 ) ;
#47317=DIRECTION ( 'NONE',  ( 1.073024830501117725E-15, -6.982962677686266711E-15, 1.000000000000000000 ) ) ;
#47536=VECTOR ( 'NONE', #86772, 1000.000000000000000 ) ;
#47790=CARTESIAN_POINT ( 'NONE',  ( -16.77431908686106965, 66.05419424549431540, -157.3589467021746486 ) ) ;
#48009=LINE ( 'NONE', #106689, #82308 ) ;
#48086=DIRECTION ( 'NONE',  ( 0.000000000000000000, 6.982962677686266711E-15, -1.000000000000000000 ) ) ;
#48212=( GEOMETRIC_REPRESENTATION_CONTEXT ( 3 ) GLOBAL_UNCERTAINTY_ASSIGNED_CONTEXT ( ( #201743 ) ) GLOBAL_UNIT_ASSIGNED_CONTEXT ( ( #93212, #172805, #194912 ) ) REPRESENTATION_CONTEXT ( 'NONE', 'WORKASPACE' ) );
#48358=VERTEX_POINT ( 'NONE', #218112 ) ;
#48383=CARTESIAN_POINT ( 'NONE',  ( -16.87036670365549895, 66.01058118071065905, -157.5026676018264880 ) ) ;
#48564=LINE ( 'NONE', #73303, #39896 ) ;
#48590=EDGE_CURVE ( 'NONE', #151632, #13430, #243507, .T. ) ;
#48709=CARTESIAN_POINT ( 'NONE',  ( -15.73854595235691534, 66.64858632091087998, -153.0427639169753604 ) ) ;
#49102=DIRECTION ( 'NONE',  ( 1.000000000000000000, 0.000000000000000000, 0.000000000000000000 ) ) ;
#49218=CARTESIAN_POINT ( 'NONE',  ( -16.88853107394619357, 66.04912151666525233, -149.1701711376321953 ) ) ;
#49288=CARTESIAN_POINT ( 'NONE',  ( -18.39999999999999858, 64.25000000001233502, -160.7731074845244450 ) ) ;
#49530=EDGE_LOOP ( 'NONE', ( #176223, #235542, #37231, #79658 ) ) ;
#49749=DIRECTION ( 'NONE',  ( 0.5932847527679310229, 0.8049926720990042694, 6.257843056355992909E-15 ) ) ;
#49844=ORIENTED_EDGE ( 'NONE', *, *, #135624, .F. ) ;
#50065=VECTOR ( 'NONE', #117286, 1000.000000000000000 ) ;
#50352=CARTESIAN_POINT ( 'NONE',  ( -16.85722902420150504, 66.05000000001230376, -157.2575600107541050 ) ) ;
#50586=CARTESIAN_POINT ( 'NONE',  ( -17.05016517655713670, 66.05000000001231797, -157.3504094885308007 ) ) ;
#50588=CARTESIAN_POINT ( 'NONE',  ( 15.70340296795548873, 66.64411154550971617, -153.7344645877463734 ) ) ;
#50973=CARTESIAN_POINT ( 'NONE',  ( -16.77180007708462028, 66.05000000001224691, -149.1587216034792505 ) ) ;
#50983=CARTESIAN_POINT ( 'NONE',  ( 12.84435279558019793, 66.58929125296516816, -151.9538990786803367 ) ) ;
#51038=DIRECTION ( 'NONE',  ( -1.186688945009010077E-16, -1.000000000000000000, -7.759275652592821052E-15 ) ) ;
#51676=ADVANCED_FACE ( 'NONE', ( #60630 ), #236702, .F. ) ;
#51702=CARTESIAN_POINT ( 'NONE',  ( -13.54795643572458808, 66.54933111084471875, -154.9675609943170400 ) ) ;
#51716=ORIENTED_EDGE ( 'NONE', *, *, #28131, .F. ) ;
#51869=CARTESIAN_POINT ( 'NONE',  ( 14.87567385445977131, 66.56923500458995591, -154.7925700897740455 ) ) ;
#52165=DIRECTION ( 'NONE',  ( -0.000000000000000000, -6.982962677686266711E-15, 1.000000000000000000 ) ) ;
#52227=DIRECTION ( 'NONE',  ( -1.020425574104004196E-15, -6.982962677686266711E-15, 1.000000000000000000 ) ) ;
#52265=CARTESIAN_POINT ( 'NONE',  ( -16.87683809663752399, 66.15000000001225544, -149.9254715027207396 ) ) ;
#52277=CARTESIAN_POINT ( 'NONE',  ( 13.88638282980483929, 66.54257354752334663, -151.5230656161243985 ) ) ;
#52301=EDGE_CURVE ( 'NONE', #139384, #107287, #208833, .T. ) ;
#52352=EDGE_CURVE ( 'NONE', #222558, #24865, #141811, .T. ) ;
#52416=CARTESIAN_POINT ( 'NONE',  ( 22.88900146558018989, 67.29609520889948726, -157.3731074845244109 ) ) ;
#52871=CIRCLE ( 'NONE', #215200, 0.1000000000000028644 ) ;
#52897=ADVANCED_FACE ( 'NONE', ( #224966 ), #200297, .F. ) ;
#53076=FACE_OUTER_BOUND ( 'NONE', #158315, .T. ) ;
#53181=CARTESIAN_POINT ( 'NONE',  ( -17.11825945287481687, 65.95000000001225260, -149.1731074845244507 ) ) ;
#53212=( BOUNDED_SURFACE ( )  B_SPLINE_SURFACE ( 3, 2, ( 
 ( #52265, #194393, #133116 ),
 ( #56117, #113545, #233514 ),
 ( #130534, #193096, #190541 ),
 ( #152709, #213930, #95264 ),
 ( #35335, #169713, #10604 ),
 ( #173576, #210098, #135658 ),
 ( #134369, #171006, #92688 ),
 ( #172286, #114827, #251772 ),
 ( #110980, #230953, #36613 ),
 ( #131820, #73170, #50973 ) ),
 .UNSPECIFIED., .F., .F., .F. ) 
 B_SPLINE_SURFACE_WITH_KNOTS ( ( 4, 2, 2, 2, 4 ),
 ( 3, 3 ),
 ( 0.002161241639767276426, 0.002579950749615843482, 0.002789305304540127227, 0.002893982582002269099, 0.002998659859464410972 ),
 ( 0.000000000000000000, 1.000000000000000000 ),
 .UNSPECIFIED. ) 
 GEOMETRIC_REPRESENTATION_ITEM ( )  RATIONAL_B_SPLINE_SURFACE ( (
 ( 1.000000000000000000, 0.7071067811865475727, 1.000000000000000000),
 ( 1.000000000000000000, 0.7632447400667128345, 1.000000000000000000),
 ( 1.000000000000000000, 0.8158073005106601938, 1.000000000000000000),
 ( 1.000000000000000000, 0.8906973462397633767, 1.000000000000000000),
 ( 1.000000000000000000, 0.9149408947802050163, 1.000000000000000000),
 ( 1.000000000000000000, 0.9493368785274935995, 1.000000000000000000),
 ( 1.000000000000000000, 0.9605194247158138632, 1.000000000000000000),
 ( 1.000000000000000000, 0.9803630264779780168, 1.000000000000000000),
 ( 1.000000000000000000, 0.9900844824272214684, 1.000000000000000000),
 ( 1.000000000000000000, 0.9894588281429246290, 1.000000000000000000) ) ) 
 REPRESENTATION_ITEM ( '' )  SURFACE ( )  );
#53222=CARTESIAN_POINT ( 'NONE',  ( -16.94445028196807002, 66.00793639031451221, -149.1304376629428816 ) ) ;
#53328=ORIENTED_EDGE ( 'NONE', *, *, #108051, .T. ) ;
#53441=ORIENTED_EDGE ( 'NONE', *, *, #229237, .F. ) ;
#53521=ORIENTED_EDGE ( 'NONE', *, *, #248400, .T. ) ;
#53606=VERTEX_POINT ( 'NONE', #133302 ) ;
#53868=VERTEX_POINT ( 'NONE', #109240 ) ;
#54119=CARTESIAN_POINT ( 'NONE',  ( -17.80356949363524777, 65.12326860301459419, -159.7361805087439279 ) ) ;
#54141=EDGE_LOOP ( 'NONE', ( #87778, #180061, #3116, #167527 ) ) ;
#54200=CARTESIAN_POINT ( 'NONE',  ( 18.54999999999999716, 67.25000000001227818, -157.3731074845244393 ) ) ;
#54222=CARTESIAN_POINT ( 'NONE',  ( -16.77779411503079388, 66.05389855308817459, -157.3600500669045914 ) ) ;
#54246=CIRCLE ( 'NONE', #216575, 0.09999999999999939493 ) ;
#54345=EDGE_CURVE ( 'NONE', #221781, #189976, #59192, .T. ) ;
#54500=LINE ( 'NONE', #33709, #146291 ) ;
#54535=DIRECTION ( 'NONE',  ( 0.000000000000000000, -1.000000000000000000, -6.982962677686266711E-15 ) ) ;
#54587=PLANE ( 'NONE',  #257375 ) ;
#54919=ORIENTED_EDGE ( 'NONE', *, *, #156602, .T. ) ;
#54937=EDGE_CURVE ( 'NONE', #184435, #24761, #86169, .T. ) ;
#54990=CARTESIAN_POINT ( 'NONE',  ( -16.80100914604134843, 66.05685090590866082, -149.2060633572367863 ) ) ;
#55081=CARTESIAN_POINT ( 'NONE',  ( -16.97683809663752186, 66.05000000001230376, -156.6207434663279514 ) ) ;
#55151=DIRECTION ( 'NONE',  ( -1.000000000000000000, 0.000000000000000000, -0.000000000000000000 ) ) ;
#55231=AXIS2_PLACEMENT_3D ( 'NONE', #228918, #89387, #72426 ) ;
#55337=( NAMED_UNIT ( * ) SI_UNIT ( $, .STERADIAN. ) SOLID_ANGLE_UNIT ( ) );
#55461=AXIS2_PLACEMENT_3D ( 'NONE', #27013, #229045, #49102 ) ;
#55588=VECTOR ( 'NONE', #119396, 1000.000000000000000 ) ;
#55704=CARTESIAN_POINT ( 'NONE',  ( -16.92209698673614326, 66.05000000001224691, -149.2337430515783581 ) ) ;
#55844=FACE_OUTER_BOUND ( 'NONE', #189846, .T. ) ;
#55934=ORIENTED_EDGE ( 'NONE', *, *, #99174, .T. ) ;
#56080=CARTESIAN_POINT ( 'NONE',  ( -17.80356949364090013, 65.12326860300883880, -146.8100344602939060 ) ) ;
#56117=CARTESIAN_POINT ( 'NONE',  ( -16.87683809663752399, 66.13411015067987364, -149.7905342915939855 ) ) ;
#56171=CARTESIAN_POINT ( 'NONE',  ( 12.25000000000000000, 66.65000000001228386, -153.2731074845244166 ) ) ;
#56214=VERTEX_POINT ( 'NONE', #97766 ) ;
#56516=ADVANCED_FACE ( 'NONE', ( #119111 ), #79935, .F. ) ;
#56585=CARTESIAN_POINT ( 'NONE',  ( -16.94107738177415712, 65.98576071487568129, -157.4731074845244336 ) ) ;
#56621=SURFACE_STYLE_FILL_AREA ( #114054 ) ;
#56671=CARTESIAN_POINT ( 'NONE',  ( -14.00000000000000178, 66.15000000001228386, -153.2731074845244166 ) ) ;
#56713=ADVANCED_FACE ( 'NONE', ( #86035 ), #130317, .F. ) ;
#56739=DIRECTION ( 'NONE',  ( 0.000000000000000000, -6.982962677686266711E-15, 1.000000000000000000 ) ) ;
#56817=ORIENTED_EDGE ( 'NONE', *, *, #44734, .F. ) ;
#56966=EDGE_CURVE ( 'NONE', #254732, #80617, #90011, .T. ) ;
#57124=DIRECTION ( 'NONE',  ( -1.000000000000000000, 0.000000000000000000, 0.000000000000000000 ) ) ;
#57198=LINE ( 'NONE', #59763, #3670 ) ;
#57374=EDGE_CURVE ( 'NONE', #53868, #42338, #223457, .T. ) ;
#57568=CARTESIAN_POINT ( 'NONE',  ( -16.79140778683511215, 66.05505840115770866, -149.1933702507536736 ) ) ;
#57691=CARTESIAN_POINT ( 'NONE',  ( -33.72168855820452649, 52.34166666667894674, -153.2731074845245303 ) ) ;
#57939=ORIENTED_EDGE ( 'NONE', *, *, #45729, .F. ) ;
#58026=EDGE_CURVE ( 'NONE', #161169, #67174, #68760, .T. ) ;
#58077=CARTESIAN_POINT ( 'NONE',  ( -15.55912972643741199, 67.50912972644972854, -157.4731074845244336 ) ) ;
#58203=DIRECTION ( 'NONE',  ( -1.000000000000000000, 0.000000000000000000, 0.000000000000000000 ) ) ;
#58390=ORIENTED_EDGE ( 'NONE', *, *, #22460, .T. ) ;
#58640=CYLINDRICAL_SURFACE ( 'NONE', #203447, 0.09999999999999939493 ) ;
#58648=FACE_OUTER_BOUND ( 'NONE', #111194, .T. ) ;
#58733=LINE ( 'NONE', #120054, #176098 ) ;
#58770=CARTESIAN_POINT ( 'NONE',  ( 20.73486653747088582, 68.75000000001229239, -160.7731074845244166 ) ) ;
#58960=VERTEX_POINT ( 'NONE', #244248 ) ;
#59001=VERTEX_POINT ( 'NONE', #9499 ) ;
#59192=LINE ( 'NONE', #38394, #151106 ) ;
#59255=CARTESIAN_POINT ( 'NONE',  ( -18.34374000495060386, 64.52683809664983983, -160.7731074845244450 ) ) ;
#59301=DIRECTION ( 'NONE',  ( 1.000000000000000000, 0.000000000000000000, 0.000000000000000000 ) ) ;
#59333=PLANE ( 'NONE',  #94480 ) ;
#59441=DIRECTION ( 'NONE',  ( 0.000000000000000000, 0.000000000000000000, 1.000000000000000000 ) ) ;
#59452=EDGE_CURVE ( 'NONE', #114211, #46041, #201009, .T. ) ;
#59609=DIRECTION ( 'NONE',  ( -0.000000000000000000, -6.982962677686266711E-15, 1.000000000000000000 ) ) ;
#59755=CARTESIAN_POINT ( 'NONE',  ( -15.55912972643741199, 67.50912972644972854, -157.3731074845244109 ) ) ;
#59763=CARTESIAN_POINT ( 'NONE',  ( -16.27683809663751191, 66.65000000001232650, -157.4731074845244336 ) ) ;
#59779=FACE_OUTER_BOUND ( 'NONE', #11838, .T. ) ;
#59846=VECTOR ( 'NONE', #159075, 1000.000000000000000 ) ;
#59976=CARTESIAN_POINT ( 'NONE',  ( 23.24999999999999645, 70.35000000001230092, -157.3731074845244109 ) ) ;
#60022=ORIENTED_EDGE ( 'NONE', *, *, #6358, .F. ) ;
#60036=CARTESIAN_POINT ( 'NONE',  ( 20.09999999999999787, 66.25000000001227818, -149.1731074845244223 ) ) ;
#60051=( BOUNDED_CURVE ( )  B_SPLINE_CURVE ( 3, ( #33571, #193892, #73967, #115626 ),
 .UNSPECIFIED., .F., .F. ) 
 B_SPLINE_CURVE_WITH_KNOTS ( ( 4, 4 ),
 ( 5.731445031868798168, 5.983100554402348337 ),
 .UNSPECIFIED. ) 
 CURVE ( )  GEOMETRIC_REPRESENTATION_ITEM ( )  RATIONAL_B_SPLINE_CURVE ( ( 1.000000000000000000, 0.9947294176030464508, 0.9947294176030464508, 1.000000000000000000 ) ) 
 REPRESENTATION_ITEM ( '' )  );
#60183=EDGE_CURVE ( 'NONE', #80617, #254732, #167186, .T. ) ;
#60269=EDGE_CURVE ( 'NONE', #139384, #62835, #54500, .T. ) ;
#60393=FACE_OUTER_BOUND ( 'NONE', #78385, .T. ) ;
#60509=CARTESIAN_POINT ( 'NONE',  ( -16.89021194854739605, 66.05000000001224691, -149.2805393529200728 ) ) ;
#60521=EDGE_CURVE ( 'NONE', #68090, #80528, #107746, .T. ) ;
#60563=CARTESIAN_POINT ( 'NONE',  ( -12.33960340485503870, 66.63925083009715422, -152.7085373439171576 ) ) ;
#60630=FACE_OUTER_BOUND ( 'NONE', #4701, .T. ) ;
#60926=AXIS2_PLACEMENT_3D ( 'NONE', #234182, #34741, #218464 ) ;
#60948=CARTESIAN_POINT ( 'NONE',  ( -16.89155683852408174, 66.05000000001230376, -156.7457356349848681 ) ) ;
#61012=CARTESIAN_POINT ( 'NONE',  ( 21.72449340488910607, 65.71604372252119219, -160.7731074845244166 ) ) ;
#61424=ORIENTED_EDGE ( 'NONE', *, *, #65148, .T. ) ;
#61455=CARTESIAN_POINT ( 'NONE',  ( 21.72449340488910252, 65.71604372252116377, -157.3731074845244393 ) ) ;
#61461=CARTESIAN_POINT ( 'NONE',  ( -18.40000000000000213, 70.35000000001230092, -157.3731074845244109 ) ) ;
#61464=CARTESIAN_POINT ( 'NONE',  ( -16.98495255085918032, 65.99443563401753465, -157.3884902783039195 ) ) ;
#61774=CARTESIAN_POINT ( 'NONE',  ( -16.93440969289730802, 66.00481482419834833, -157.4318732995136259 ) ) ;
#61783=CIRCLE ( 'NONE', #219995, 0.9000000000000014655 ) ;
#62222=DIRECTION ( 'NONE',  ( 0.000000000000000000, 1.000000000000000000, 6.982962677686266711E-15 ) ) ;
#62245=CARTESIAN_POINT ( 'NONE',  ( -16.84981964351479533, 66.08268176591360543, -157.1535058705049153 ) ) ;
#62286=CARTESIAN_POINT ( 'NONE',  ( -14.00000000000000178, 66.15000000001228386, -153.2731074845244166 ) ) ;
#62315=CARTESIAN_POINT ( 'NONE',  ( -14.23072895065543975, 66.54401276639954688, -155.0115763176265489 ) ) ;
#62835=VERTEX_POINT ( 'NONE', #60036 ) ;
#62894=STYLED_ITEM ( 'NONE', ( #63772 ), #194237 ) ;
#63019=ORIENTED_EDGE ( 'NONE', *, *, #108051, .F. ) ;
#63038=CARTESIAN_POINT ( 'NONE',  ( -16.97683809663753252, 66.05000000001230376, -156.7515827158544823 ) ) ;
#63046=CARTESIAN_POINT ( 'NONE',  ( -16.93906926870270624, 65.98785312906574063, -157.4696551772975965 ) ) ;
#63128=CARTESIAN_POINT ( 'NONE',  ( -12.92414019175887141, 66.58236703690597835, -151.8741590187921133 ) ) ;
#63419=CARTESIAN_POINT ( 'NONE',  ( 23.24999999999999645, 64.25000000001230660, -157.3731074845244393 ) ) ;
#63439=CARTESIAN_POINT ( 'NONE',  ( -20.65000000000000568, 68.75000000001233502, -160.7731074845244166 ) ) ;
#63628=CARTESIAN_POINT ( 'NONE',  ( -16.87683809663752399, 54.76195096157923103, -157.3731074845245246 ) ) ;
#63772=PRESENTATION_STYLE_ASSIGNMENT (( #242402 ) ) ;
#64191=CARTESIAN_POINT ( 'NONE',  ( 18.39999999999999503, 64.52683809664981140, -157.3731074845244393 ) ) ;
#64326=ORIENTED_EDGE ( 'NONE', *, *, #233668, .T. ) ;
#64338=ADVANCED_FACE ( 'NONE', ( #137719 ), #77745, .T. ) ;
#64686=CARTESIAN_POINT ( 'NONE',  ( -16.27683809663750480, 66.65000000001225544, -149.0731074845244279 ) ) ;
#64751=AXIS2_PLACEMENT_3D ( 'NONE', #132264, #211817, #13612 ) ;
#64802=CARTESIAN_POINT ( 'NONE',  ( -16.87683809663752399, 66.15000000001232650, -156.6207434663279230 ) ) ;
#64876=CYLINDRICAL_SURFACE ( 'NONE', #72357, 0.09999999999998898659 ) ;
#64914=CARTESIAN_POINT ( 'NONE',  ( -18.40000000000000213, 64.66825945288714195, -157.3731074845244393 ) ) ;
#64939=ORIENTED_EDGE ( 'NONE', *, *, #86325, .T. ) ;
#65001=LINE ( 'NONE', #45446, #95799 ) ;
#65030=CARTESIAN_POINT ( 'NONE',  ( -16.87242674293850087, 66.05000000001231797, -157.3741977308967819 ) ) ;
#65058=EDGE_LOOP ( 'NONE', ( #11430, #40977, #134461, #183037 ) ) ;
#65116=DIRECTION ( 'NONE',  ( 0.8049926720990051576, -0.5932847527679298016, -4.142885285818778274E-15 ) ) ;
#65148=EDGE_CURVE ( 'NONE', #251500, #53868, #10940, .T. ) ;
#65196=LINE ( 'NONE', #104303, #7813 ) ;
#65212=VECTOR ( 'NONE', #224905, 1000.000000000000000 ) ;
#65316=FACE_OUTER_BOUND ( 'NONE', #2070, .T. ) ;
#65497=B_SPLINE_CURVE_WITH_KNOTS ( 'NONE', 3,
 ( #20134, #219589, #239170, #60509, #81341, #180485, #202610, #124368, #541, #203884 ),
 .UNSPECIFIED., .F., .F.,
 ( 4, 2, 2, 2, 4 ),
 ( 5.134898698599272065E-16, 9.930191194498475427E-05, 0.0001986038238894560033, 0.0003972076477783985284, 0.0007944152955562835787 ),
 .UNSPECIFIED. ) ;
#65612=CARTESIAN_POINT ( 'NONE',  ( -16.86132326855785735, 66.05000000001230376, -157.3244716998561046 ) ) ;
#65681=EDGE_CURVE ( 'NONE', #58960, #4697, #209303, .T. ) ;
#66170=DIRECTION ( 'NONE',  ( -1.000000000000000000, 0.000000000000000000, -0.000000000000000000 ) ) ;
#66268=CARTESIAN_POINT ( 'NONE',  ( 20.99999999999999645, 66.25000000001226397, -149.1731074845244223 ) ) ;
#66751=CARTESIAN_POINT ( 'NONE',  ( -21.65000000000000213, 68.75000000001233502, -160.7731074845244166 ) ) ;
#66761=ADVANCED_FACE ( 'NONE', ( #106379 ), #245922, .F. ) ;
#66822=AXIS2_PLACEMENT_3D ( 'NONE', #182436, #85850, #187580 ) ;
#66846=EDGE_LOOP ( 'NONE', ( #188009, #139477, #27232, #12909, #213620 ) ) ;
#66859=ADVANCED_FACE ( 'NONE', ( #91966 ), #121061, .T. ) ;
#66900=CARTESIAN_POINT ( 'NONE',  ( -16.90137573187933739, 66.05000000001230376, -157.2346900604275390 ) ) ;
#66997=ORIENTED_EDGE ( 'NONE', *, *, #89019, .F. ) ;
#66998=CARTESIAN_POINT ( 'NONE',  ( -15.57281606413132025, 66.62934494888880010, -152.4972842285435206 ) ) ;
#67174=VERTEX_POINT ( 'NONE', #126944 ) ;
#67232=CARTESIAN_POINT ( 'NONE',  ( -16.77683809663752257, 52.34166666667894674, -153.2731074845245303 ) ) ;
#67253=CARTESIAN_POINT ( 'NONE',  ( -18.40000000000000213, 64.58541674041249792, -157.3731074845244677 ) ) ;
#67274=CARTESIAN_POINT ( 'NONE',  ( 13.99999999999999822, 66.15000000001228386, -153.2731074845244450 ) ) ;
#67341=CARTESIAN_POINT ( 'NONE',  ( -33.72168855820452649, 64.52683809664983983, -160.7731074845244450 ) ) ;
#67543=DIRECTION ( 'NONE',  ( 1.073024830501117725E-15, -6.982962677686266711E-15, 1.000000000000000000 ) ) ;
#67597=VERTEX_POINT ( 'NONE', #166167 ) ;
#67786=ORIENTED_EDGE ( 'NONE', *, *, #242275, .T. ) ;
#67788=VECTOR ( 'NONE', #192389, 999.9999999999998863 ) ;
#68090=VERTEX_POINT ( 'NONE', #108426 ) ;
#68276=EDGE_CURVE ( 'NONE', #221781, #246673, #220371, .T. ) ;
#68453=AXIS2_PLACEMENT_3D ( 'NONE', #187451, #127462, #148313 ) ;
#68521=VECTOR ( 'NONE', #59301, 1000.000000000000000 ) ;
#68568=CARTESIAN_POINT ( 'NONE',  ( -16.91256925476571737, 66.01426884188410327, -157.4907499735297449 ) ) ;
#68736=CARTESIAN_POINT ( 'NONE',  ( -12.93407622233968546, 66.58221053306007775, -154.6657229405475391 ) ) ;
#68760=B_SPLINE_CURVE_WITH_KNOTS ( 'NONE', 3,
 ( #70756, #150277, #152870, #109835, #112435, #10756, #231107, #210252, #108569, #229794 ),
 .UNSPECIFIED., .F., .F.,
 ( 4, 3, 3, 4 ),
 ( 1.950915401637565782E-15, 8.145022132826850876E-06, 1.905645951092260044E-05, 2.061107371225642508E-05 ),
 .UNSPECIFIED. ) ;
#68785=EDGE_CURVE ( 'NONE', #151479, #189963, #175876, .T. ) ;
#68854=FACE_OUTER_BOUND ( 'NONE', #181702, .T. ) ;
#69118=CARTESIAN_POINT ( 'NONE',  ( -16.91256925476570672, 66.01426884188404642, -149.0554649955191735 ) ) ;
#69189=EDGE_LOOP ( 'NONE', ( #61424, #144326, #84576, #122176 ) ) ;
#69295=DIRECTION ( 'NONE',  ( 0.000000000000000000, 6.982962677686266711E-15, -1.000000000000000000 ) ) ;
#69312=CARTESIAN_POINT ( 'NONE',  ( 12.93279065517213766, 66.58230930894914934, -151.8815067877598608 ) ) ;
#69346=DIRECTION ( 'NONE',  ( -1.000000000000000000, 1.646408749285562691E-14, 1.149681084847720908E-28 ) ) ;
#69555=ORIENTED_EDGE ( 'NONE', *, *, #157157, .T. ) ;
#69587=CARTESIAN_POINT ( 'NONE',  ( -15.75000000000000355, 66.65000000001229807, -153.1588398769083028 ) ) ;
#69724=LINE ( 'NONE', #227482, #111917 ) ;
#69967=CARTESIAN_POINT ( 'NONE',  ( -16.77308656112214891, 66.05000000001228955, -157.3729142928221165 ) ) ;
#70422=CARTESIAN_POINT ( 'NONE',  ( -16.92570016628982543, 66.04121104227236572, -149.1437581545634430 ) ) ;
#70504=CARTESIAN_POINT ( 'NONE',  ( -16.87331047859649757, 66.05000000001224691, -149.1731074845244223 ) ) ;
#70756=CARTESIAN_POINT ( 'NONE',  ( -16.89268316805466341, 66.04827818677011919, -157.3788599630699707 ) ) ;
#70847=CARTESIAN_POINT ( 'NONE',  ( -18.40000000000000213, 70.35000000001224407, -149.1731074845243938 ) ) ;
#70870=CARTESIAN_POINT ( 'NONE',  ( 23.24999999999999645, 64.25000000001224976, -149.1731074845244507 ) ) ;
#71130=EDGE_LOOP ( 'NONE', ( #114662, #147892, #166605, #69555 ) ) ;
#71212=DIRECTION ( 'NONE',  ( 1.000000000000000000, 0.000000000000000000, 0.000000000000000000 ) ) ;
#71250=CARTESIAN_POINT ( 'NONE',  ( -16.79270642812249292, 66.05375578307356932, -157.3620407630891123 ) ) ;
#71282=AXIS2_PLACEMENT_3D ( 'NONE', #171047, #210133, #26689 ) ;
#71559=EDGE_CURVE ( 'NONE', #13430, #230269, #184500, .T. ) ;
#71827=CARTESIAN_POINT ( 'NONE',  ( -18.40000000000000213, 64.52683809665026615, -145.8229367329901436 ) ) ;
#72353=PRODUCT ( 'Snap Open Cable Crossbars 12', 'Snap Open Cable Crossbars 12', '', ( #133060 ) ) ;
#72357=AXIS2_PLACEMENT_3D ( 'NONE', #4880, #66170, #244794 ) ;
#72395=( LENGTH_UNIT ( ) NAMED_UNIT ( * ) SI_UNIT ( .MILLI., .METRE. ) );
#72426=DIRECTION ( 'NONE',  ( 0.5932847527679310229, 0.8049926720990042694, 5.621233785078285907E-15 ) ) ;
#72734=EDGE_LOOP ( 'NONE', ( #66997, #9098, #116797, #180651, #185936 ) ) ;
#72910=DIRECTION ( 'NONE',  ( 0.000000000000000000, 6.982962677686266711E-15, -1.000000000000000000 ) ) ;
#72984=CARTESIAN_POINT ( 'NONE',  ( -16.89797118371622275, 66.02361927736751568, -149.0858141169672706 ) ) ;
#73077=CARTESIAN_POINT ( 'NONE',  ( -16.92507428761699018, 66.05000000001224691, -149.2365049441459917 ) ) ;
#73102=ORIENTED_EDGE ( 'NONE', *, *, #68276, .T. ) ;
#73144=DIRECTION ( 'NONE',  ( 0.2834754621636439431, 0.2834754621636471628, 0.9161240771326858434 ) ) ;
#73170=CARTESIAN_POINT ( 'NONE',  ( -16.77308656112215246, 66.05000000001226113, -149.1733006762267451 ) ) ;
#73182=CARTESIAN_POINT ( 'NONE',  ( 12.60873083341399159, 66.61042836546585022, -152.2054667721552335 ) ) ;
#73235=EDGE_CURVE ( 'NONE', #53868, #105637, #155269, .T. ) ;
#73292=LINE ( 'NONE', #119788, #122348 ) ;
#73303=CARTESIAN_POINT ( 'NONE',  ( 18.39999999999999503, 70.35000000001230092, -157.3731074845244109 ) ) ;
#73310=EDGE_CURVE ( 'NONE', #132836, #111853, #84815, .T. ) ;
#73415=DIRECTION ( 'NONE',  ( 1.000000000000000000, 0.000000000000000000, 0.000000000000000000 ) ) ;
#73693=ORIENTED_EDGE ( 'NONE', *, *, #54937, .T. ) ;
#73939=FACE_OUTER_BOUND ( 'NONE', #233590, .T. ) ;
#73944=VECTOR ( 'NONE', #234922, 1000.000000000000000 ) ;
#73967=CARTESIAN_POINT ( 'NONE',  ( -17.22361732159832215, 65.65484434140988412, -158.6523229586572938 ) ) ;
#74470=CARTESIAN_POINT ( 'NONE',  ( 12.48201962039797408, 66.62334006147874277, -152.3949149363072024 ) ) ;
#74669=CARTESIAN_POINT ( 'NONE',  ( -16.97683809663752186, 66.05000000001233218, -160.7731074845244166 ) ) ;
#74851=CIRCLE ( 'NONE', #116518, 0.1000000000000028644 ) ;
#75006=CARTESIAN_POINT ( 'NONE',  ( 21.72449340488910607, 65.71604372252112114, -149.1731074845244507 ) ) ;
#75065=ORIENTED_EDGE ( 'NONE', *, *, #85161, .F. ) ;
#75157=FACE_OUTER_BOUND ( 'NONE', #233808, .T. ) ;
#75592=LINE ( 'NONE', #135516, #94118 ) ;
#75695=DIRECTION ( 'NONE',  ( 1.186688945009010077E-16, 1.000000000000000000, 6.982962677686266711E-15 ) ) ;
#75750=VECTOR ( 'NONE', #139225, 1000.000000000000000 ) ;
#76046=ORIENTED_EDGE ( 'NONE', *, *, #3437, .F. ) ;
#76345=CARTESIAN_POINT ( 'NONE',  ( -18.40000000000000213, 64.25000000001224976, -149.1731074845244507 ) ) ;
#76470=ORIENTED_EDGE ( 'NONE', *, *, #88654, .F. ) ;
#76492=ORIENTED_EDGE ( 'NONE', *, *, #25986, .T. ) ;
#76645=EDGE_CURVE ( 'NONE', #2008, #210270, #234220, .T. ) ;
#76674=CARTESIAN_POINT ( 'NONE',  ( -16.92563707711778775, 66.03100930561545567, -149.1423491850004552 ) ) ;
#76800=ORIENTED_EDGE ( 'NONE', *, *, #121162, .T. ) ;
#77028=CARTESIAN_POINT ( 'NONE',  ( 13.76927104934457624, 66.54401276639956109, -155.0115763176266341 ) ) ;
#77031=CARTESIAN_POINT ( 'NONE',  ( -18.34374000495059676, 64.52683809664972614, -145.7731074845244450 ) ) ;
#77142=CARTESIAN_POINT ( 'NONE',  ( -16.81931177881022066, 66.06300394050835223, -149.2498896059072422 ) ) ;
#77254=DIRECTION ( 'NONE',  ( 1.020425574104004196E-15, -6.982962677686266711E-15, 1.000000000000000000 ) ) ;
#77361=EDGE_CURVE ( 'NONE', #224786, #96826, #16841, .T. ) ;
#77397=VERTEX_POINT ( 'NONE', #196736 ) ;
#77727=DIRECTION ( 'NONE',  ( -1.000000000000000000, 1.186688945009010077E-16, 8.286604613020808509E-31 ) ) ;
#77745=CYLINDRICAL_SURFACE ( 'NONE', #239324, 0.09999999999998898659 ) ;
#77768=CARTESIAN_POINT ( 'NONE',  ( -16.97683809663752186, 66.15000000001231228, -156.6207434663279230 ) ) ;
#77831=VECTOR ( 'NONE', #169874, 1000.000000000000000 ) ;
#77953=CARTESIAN_POINT ( 'NONE',  ( -16.93301857435208291, 66.02369064527677267, -149.1373319133629423 ) ) ;
#78115=AXIS2_PLACEMENT_3D ( 'NONE', #144988, #109716, #246664 ) ;
#78152=PLANE ( 'NONE',  #199356 ) ;
#78385=EDGE_LOOP ( 'NONE', ( #2155, #58390, #150549, #183213, #247661, #54919 ) ) ;
#78425=CARTESIAN_POINT ( 'NONE',  ( -16.81453563122428108, 66.06089979457530603, -149.2348488238791901 ) ) ;
#78580=CARTESIAN_POINT ( 'NONE',  ( 20.05000000000002913, 68.75000000001222134, -149.1731074845244223 ) ) ;
#78709=CARTESIAN_POINT ( 'NONE',  ( -16.81744102076748959, 66.05000000001224691, -149.1731074845244223 ) ) ;
#78845=CARTESIAN_POINT ( 'NONE',  ( -18.37160782347004329, 64.52438358520993233, -160.7731074845244450 ) ) ;
#79015=CARTESIAN_POINT ( 'NONE',  ( -23.25000000000000355, 65.95000000001230944, -157.2731074845244166 ) ) ;
#79278=CYLINDRICAL_SURFACE ( 'NONE', #194755, 1.749999999999999778 ) ;
#79291=CARTESIAN_POINT ( 'NONE',  ( -16.88495309932524080, 66.04537294153944060, -157.3885588107125386 ) ) ;
#79353=CARTESIAN_POINT ( 'NONE',  ( 18.39999999999999503, 70.35000000001230092, -157.3731074845244109 ) ) ;
#79414=LINE ( 'NONE', #239808, #50065 ) ;
#79446=ORIENTED_EDGE ( 'NONE', *, *, #186062, .T. ) ;
#79658=ORIENTED_EDGE ( 'NONE', *, *, #216098, .F. ) ;
#79736=LINE ( 'NONE', #74669, #12495 ) ;
#79750=ORIENTED_EDGE ( 'NONE', *, *, #221889, .T. ) ;
#79802=CARTESIAN_POINT ( 'NONE',  ( 23.24999999999999645, 70.35000000001224407, -149.1731074845243938 ) ) ;
#79845=( BOUNDED_CURVE ( )  B_SPLINE_CURVE ( 3, ( #116127, #17031, #159119, #157853 ),
 .UNSPECIFIED., .F., .F. ) 
 B_SPLINE_CURVE_WITH_KNOTS ( ( 4, 4 ),
 ( 3.432212674861197854, 3.693332928900581180 ),
 .UNSPECIFIED. ) 
 CURVE ( )  GEOMETRIC_REPRESENTATION_ITEM ( )  RATIONAL_B_SPLINE_CURVE ( ( 1.000000000000000000, 0.9943260843901262636, 0.9943260843901262636, 1.000000000000000000 ) ) 
 REPRESENTATION_ITEM ( '' )  );
#79935=PLANE ( 'NONE',  #114780 ) ;
#80303=AXIS2_PLACEMENT_3D ( 'NONE', #132626, #12701, #33568 ) ;
#80365=LINE ( 'NONE', #19138, #145364 ) ;
#80528=VERTEX_POINT ( 'NONE', #84243 ) ;
#80562=CARTESIAN_POINT ( 'NONE',  ( -16.86422026484316916, 66.02955263915164608, -157.4408942588514151 ) ) ;
#80617=VERTEX_POINT ( 'NONE', #257131 ) ;
#80823=ORIENTED_EDGE ( 'NONE', *, *, #73310, .T. ) ;
#80827=EDGE_CURVE ( 'NONE', #189976, #191026, #184059, .T. ) ;
#80938=ORIENTED_EDGE ( 'NONE', *, *, #7895, .F. ) ;
#81144=CARTESIAN_POINT ( 'NONE',  ( -16.77683809663752257, 66.05416425680813575, -157.3591584654202222 ) ) ;
#81152=VECTOR ( 'NONE', #110324, 1000.000000000000000 ) ;
#81161=EDGE_CURVE ( 'NONE', #56214, #3667, #22139, .T. ) ;
#81341=CARTESIAN_POINT ( 'NONE',  ( -16.90138253750127006, 66.05000000001224691, -149.3115447766198542 ) ) ;
#81498=CARTESIAN_POINT ( 'NONE',  ( -16.93658211146644987, 66.00589133767104499, -149.1188124145687652 ) ) ;
#81680=DIRECTION ( 'NONE',  ( -1.073024830501117725E-15, -6.982962677686266711E-15, 1.000000000000000000 ) ) ;
#81767=CARTESIAN_POINT ( 'NONE',  ( -16.87333278164147643, 66.11739021543357353, -156.8899396783708369 ) ) ;
#81833=CARTESIAN_POINT ( 'NONE',  ( -15.39946565075091378, 66.61046543766559580, -154.3482981801345204 ) ) ;
#81947=CARTESIAN_POINT ( 'NONE',  ( -16.89268316805466341, 66.04827818677011919, -157.3788599630699707 ) ) ;
#82291=CARTESIAN_POINT ( 'NONE',  ( -21.64999999999999858, 65.95000000001225260, -149.2731074845244450 ) ) ;
#82308=VECTOR ( 'NONE', #207104, 1000.000000000000000 ) ;
#82504=DIRECTION ( 'NONE',  ( 0.000000000000000000, -6.982962677686266711E-15, 1.000000000000000000 ) ) ;
#82583=CARTESIAN_POINT ( 'NONE',  ( -16.94445028196808778, 66.00793639031455484, -157.4157773061059800 ) ) ;
#82620=DIRECTION ( 'NONE',  ( -0.7071067811865456854, -0.7071067811865493491, -4.937700262164544098E-15 ) ) ;
#82741=LINE ( 'NONE', #227424, #111575 ) ;
#83046=CARTESIAN_POINT ( 'NONE',  ( -16.97683810757273193, 66.05000000001230376, -156.7595307720631013 ) ) ;
#83152=FACE_OUTER_BOUND ( 'NONE', #21248, .T. ) ;
#83306=SURFACE_STYLE_FILL_AREA ( #140745 ) ;
#83337=AXIS2_PLACEMENT_3D ( 'NONE', #202072, #65116, #23465 ) ;
#83338=CARTESIAN_POINT ( 'NONE',  ( -18.37013991200266361, 64.50025238380023040, -145.7300844740073273 ) ) ;
#83834=EDGE_CURVE ( 'NONE', #250417, #124544, #106747, .T. ) ;
#83941=CARTESIAN_POINT ( 'NONE',  ( -15.31895204843004521, 66.60346600605832634, -152.1171677053511075 ) ) ;
#84217=DIRECTION ( 'NONE',  ( 0.7071067811865463515, -0.7071067811865487940, -5.696443396193425170E-15 ) ) ;
#84243=CARTESIAN_POINT ( 'NONE',  ( 18.39999999999998082, 64.52683809664983983, -160.7731074845244450 ) ) ;
#84576=ORIENTED_EDGE ( 'NONE', *, *, #176292, .F. ) ;
#84676=VECTOR ( 'NONE', #35515, 1000.000000000000000 ) ;
#84754=VERTEX_POINT ( 'NONE', #207617 ) ;
#84815=LINE ( 'NONE', #121448, #236264 ) ;
#84834=DIRECTION ( 'NONE',  ( 0.000000000000000000, 6.982962677686266711E-15, -1.000000000000000000 ) ) ;
#84978=CARTESIAN_POINT ( 'NONE',  ( -16.85312841634287295, 66.08639382269207374, -157.1259343512318480 ) ) ;
#85161=EDGE_CURVE ( 'NONE', #32558, #151632, #190171, .T. ) ;
#85283=VECTOR ( 'NONE', #22893, 1000.000000000000000 ) ;
#85374=CARTESIAN_POINT ( 'NONE',  ( 18.54999999999999716, 67.25000000001229239, -160.7731074845244166 ) ) ;
#85684=CARTESIAN_POINT ( 'NONE',  ( -15.06774609480957849, 66.58234804117127226, -154.6643200920840115 ) ) ;
#85785=DIRECTION ( 'NONE',  ( 1.000000000000000000, -1.541976423090492636E-14, 0.000000000000000000 ) ) ;
#85850=DIRECTION ( 'NONE',  ( -1.073024830501117725E-15, -6.982962677686266711E-15, 1.000000000000000000 ) ) ;
#85884=EDGE_LOOP ( 'NONE', ( #169190, #254432, #170764, #35045 ) ) ;
#85918=ORIENTED_EDGE ( 'NONE', *, *, #3430, .T. ) ;
#86035=FACE_OUTER_BOUND ( 'NONE', #179414, .T. ) ;
#86169=LINE ( 'NONE', #186604, #13913 ) ;
#86325=EDGE_CURVE ( 'NONE', #46041, #189963, #98145, .T. ) ;
#86485=CARTESIAN_POINT ( 'NONE',  ( -16.87036670365548474, 65.91505003675696628, -149.0731074845244279 ) ) ;
#86612=VECTOR ( 'NONE', #106799, 1000.000000000000000 ) ;
#86772=DIRECTION ( 'NONE',  ( -1.000000000000000000, 7.492892343619937423E-30, -1.073024830501117725E-15 ) ) ;
#86787=EDGE_LOOP ( 'NONE', ( #42297, #204380 ) ) ;
#86797=CARTESIAN_POINT ( 'NONE',  ( -18.40000000000000213, 64.52683809664982562, -157.4145288407617613 ) ) ;
#86978=CARTESIAN_POINT ( 'NONE',  ( -12.25000000000000355, 66.65000000001229807, -153.5045385271217526 ) ) ;
#87365=CARTESIAN_POINT ( 'NONE',  ( 22.88900146558018989, 67.29609520889950147, -160.7731074845244166 ) ) ;
#87585=CARTESIAN_POINT ( 'NONE',  ( 20.73486653747088582, 68.75000000001229239, -160.7731074845244166 ) ) ;
#87778=ORIENTED_EDGE ( 'NONE', *, *, #107926, .F. ) ;
#88048=CARTESIAN_POINT ( 'NONE',  ( 18.39999999999999503, 64.52683809664972614, -145.7731074845244450 ) ) ;
#88295=CARTESIAN_POINT ( 'NONE',  ( -21.65000000000000213, 66.05000000001230376, -157.2731074845244166 ) ) ;
#88552=AXIS2_PLACEMENT_3D ( 'NONE', #241983, #180740, #140299 ) ;
#88640=LINE ( 'NONE', #87365, #140334 ) ;
#88654=EDGE_CURVE ( 'NONE', #111853, #45933, #249467, .T. ) ;
#88813=CARTESIAN_POINT ( 'NONE',  ( 18.39999999999999503, 70.35000000001222986, -145.7731074845243882 ) ) ;
#88831=CARTESIAN_POINT ( 'NONE',  ( 12.26145404764308999, 66.64858632091086577, -153.0427639169754173 ) ) ;
#88856=CARTESIAN_POINT ( 'NONE',  ( -23.25000000000000355, 70.35000000001224407, -149.1731074845243938 ) ) ;
#89019=EDGE_CURVE ( 'NONE', #172220, #224786, #158912, .T. ) ;
#89129=CARTESIAN_POINT ( 'NONE',  ( -15.69373346032657679, 66.64320997496638199, -152.8182809759103975 ) ) ;
#89372=DIRECTION ( 'NONE',  ( -0.7071067811865456854, -0.7071067811865493491, -4.937700262164544098E-15 ) ) ;
#89387=DIRECTION ( 'NONE',  ( -0.8049926720990042694, 0.5932847527679310229, 4.142885285818786163E-15 ) ) ;
#89552=DIRECTION ( 'NONE',  ( 1.000000000000000000, 0.000000000000000000, 0.000000000000000000 ) ) ;
#89793=LINE ( 'NONE', #213271, #146632 ) ;
#89822=DIRECTION ( 'NONE',  ( 1.186688945009009831E-16, 1.000000000000000000, 6.982962677686266711E-15 ) ) ;
#90011=CIRCLE ( 'NONE', #173280, 1.749999999999998002 ) ;
#90118=VERTEX_POINT ( 'NONE', #236053 ) ;
#90343=VECTOR ( 'NONE', #45683, 1000.000000000000000 ) ;
#90680=ADVANCED_FACE ( 'NONE', ( #180913 ), #248195, .F. ) ;
#90776=CARTESIAN_POINT ( 'NONE',  ( -16.79814274880124358, 66.05072745733498607, -157.3706744474764321 ) ) ;
#90802=TOROIDAL_SURFACE ( 'NONE', #236554, 14.20833333333334103, 0.1000000000000000056 ) ;
#90822=CARTESIAN_POINT ( 'NONE',  ( -21.65000000000000213, 68.75000000001233502, -160.7731074845244166 ) ) ;
#90911=CARTESIAN_POINT ( 'NONE',  ( -16.89268316805465986, 66.04827818677006235, -149.1673550059788909 ) ) ;
#91051=PRODUCT_DEFINITION_SHAPE ( 'NONE', 'NONE',  #29336 ) ;
#91080=CARTESIAN_POINT ( 'NONE',  ( -33.72168855820452649, 64.52683809664972614, -145.7731074845244450 ) ) ;
#91099=VECTOR ( 'NONE', #54535, 1000.000000000000000 ) ;
#91624=CARTESIAN_POINT ( 'NONE',  ( -18.39999999999999858, 64.52132590001305346, -160.7484142681837795 ) ) ;
#91885=AXIS2_PLACEMENT_3D ( 'NONE', #56671, #32044, #214490 ) ;
#91962=FACE_OUTER_BOUND ( 'NONE', #239763, .T. ) ;
#91966=FACE_OUTER_BOUND ( 'NONE', #190821, .T. ) ;
#92074=ORIENTED_EDGE ( 'NONE', *, *, #177987, .F. ) ;
#92125=ORIENTED_EDGE ( 'NONE', *, *, #8391, .T. ) ;
#92274=EDGE_LOOP ( 'NONE', ( #97315, #192155, #150446, #157930, #157352 ) ) ;
#92307=VECTOR ( 'NONE', #71212, 1000.000000000000000 ) ;
#92648=FACE_OUTER_BOUND ( 'NONE', #108129, .T. ) ;
#92688=CARTESIAN_POINT ( 'NONE',  ( -16.87401514999228169, 66.05000000001224691, -149.2430894919923219 ) ) ;
#93212=( LENGTH_UNIT ( ) NAMED_UNIT ( * ) SI_UNIT ( .MILLI., .METRE. ) );
#93353=CARTESIAN_POINT ( 'NONE',  ( -16.77977881697926321, 66.05339806647938872, -157.3617289114093865 ) ) ;
#93397=DIRECTION ( 'NONE',  ( 0.000000000000000000, -6.982962677686266711E-15, 1.000000000000000000 ) ) ;
#93455=AXIS2_PLACEMENT_3D ( 'NONE', #200390, #81680, #239521 ) ;
#93510=ORIENTED_EDGE ( 'NONE', *, *, #248400, .F. ) ;
#93823=DIRECTION ( 'NONE',  ( -1.000000000000000000, -0.000000000000000000, -0.000000000000000000 ) ) ;
#93954=ORIENTED_EDGE ( 'NONE', *, *, #121323, .T. ) ;
#93980=CARTESIAN_POINT ( 'NONE',  ( 15.66039659514496130, 66.63925083009715422, -152.7085373439171860 ) ) ;
#94118=VECTOR ( 'NONE', #230809, 1000.000000000000000 ) ;
#94480=AXIS2_PLACEMENT_3D ( 'NONE', #218424, #651, #166217 ) ;
#94546=DIRECTION ( 'NONE',  ( -1.073024830501117725E-15, 6.982962677686266711E-15, -1.000000000000000000 ) ) ;
#94568=CARTESIAN_POINT ( 'NONE',  ( -18.40000000000000213, 64.51332499825466016, -160.7731074845244450 ) ) ;
#94721=DIRECTION ( 'NONE',  ( -0.000000000000000000, -6.982962677686266711E-15, 1.000000000000000000 ) ) ;
#95264=CARTESIAN_POINT ( 'NONE',  ( -16.93710578446435377, 66.05000000001224691, -149.4419114683242640 ) ) ;
#95564=ADVANCED_FACE ( 'NONE', ( #58648 ), #25080, .T. ) ;
#95799=VECTOR ( 'NONE', #204506, 1000.000000000000000 ) ;
#95812=FACE_OUTER_BOUND ( 'NONE', #168622, .T. ) ;
#95842=CARTESIAN_POINT ( 'NONE',  ( -18.35235881385853318, 64.52658099229942934, -160.7731074845244450 ) ) ;
#96132=CARTESIAN_POINT ( 'NONE',  ( 15.52844286134409124, 66.62433047358648253, -154.1553174751384461 ) ) ;
#96157=EDGE_CURVE ( 'NONE', #210270, #96826, #230262, .T. ) ;
#96482=DIRECTION ( 'NONE',  ( -1.000000000000000000, 0.000000000000000000, 0.000000000000000000 ) ) ;
#96575=CARTESIAN_POINT ( 'NONE',  ( 12.60053434924909688, 66.61046543766556738, -154.3482981801344636 ) ) ;
#96661=CYLINDRICAL_SURFACE ( 'NONE', #187887, 0.1999999999999987899 ) ;
#96696=CARTESIAN_POINT ( 'NONE',  ( 18.54999999999999716, 67.25000000001227818, -157.3731074845244393 ) ) ;
#96826=VERTEX_POINT ( 'NONE', #214986 ) ;
#96990=CARTESIAN_POINT ( 'NONE',  ( -16.90202395485727394, 66.03405545546317512, -157.4261212057837440 ) ) ;
#97045=VECTOR ( 'NONE', #139442, 1000.000000000000000 ) ;
#97315=ORIENTED_EDGE ( 'NONE', *, *, #86325, .F. ) ;
#97766=CARTESIAN_POINT ( 'NONE',  ( -21.65000000000000213, 68.75000000001226397, -149.1731074845244223 ) ) ;
#97817=DIRECTION ( 'NONE',  ( -1.020425574104004196E-15, 6.982962677686266711E-15, -1.000000000000000000 ) ) ;
#97850=CARTESIAN_POINT ( 'NONE',  ( 12.29592348164038995, 66.64419340838213657, -153.7320049529782864 ) ) ;
#98117=CARTESIAN_POINT ( 'NONE',  ( -16.94445028196808778, 66.00793639031455484, -157.4157773061059800 ) ) ;
#98145=B_SPLINE_CURVE_WITH_KNOTS ( 'NONE', 3,
 ( #106604, #32253, #7530, #12693, #227858, #49218, #248712, #128772, #46633, #90911 ),
 .UNSPECIFIED., .F., .F.,
 ( 4, 3, 3, 4 ),
 ( 0.000000000000000000, 1.004626015991452777E-05, 1.831183478182391193E-05, 2.062343583995917743E-05 ),
 .UNSPECIFIED. ) ;
#98265=ADVANCED_FACE ( 'NONE', ( #53076 ), #136441, .F. ) ;
#98395=EDGE_LOOP ( 'NONE', ( #80823, #252055, #101086, #39686 ) ) ;
#98460=AXIS2_PLACEMENT_3D ( 'NONE', #67232, #221159, #45104 ) ;
#98491=PLANE ( 'NONE',  #60926 ) ;
#98712=VERTEX_POINT ( 'NONE', #131023 ) ;
#98917=CARTESIAN_POINT ( 'NONE',  ( -16.89268316805465986, 66.04827818677006235, -149.1673550059788909 ) ) ;
#99174=EDGE_CURVE ( 'NONE', #161169, #47223, #222650, .T. ) ;
#99545=CARTESIAN_POINT ( 'NONE',  ( -16.77828822459933633, 66.05377062495577434, -149.1857357354433589 ) ) ;
#99569=FACE_OUTER_BOUND ( 'NONE', #2350, .T. ) ;
#99783=CARTESIAN_POINT ( 'NONE',  ( -16.93433913041102912, 65.99402157848830086, -149.0877420571292760 ) ) ;
#100068=CARTESIAN_POINT ( 'NONE',  ( -16.94333152882356330, 66.00965798855456512, -149.1310759534229646 ) ) ;
#100108=CIRCLE ( 'NONE', #66822, 0.5000000000000004441 ) ;
#100234=CARTESIAN_POINT ( 'NONE',  ( -16.92132318717937522, 66.03392997600636249, -157.4007008541723565 ) ) ;
#100548=PLANE ( 'NONE',  #229206 ) ;
#100560=CARTESIAN_POINT ( 'NONE',  ( -17.01825945287481545, 66.05000000001224691, -149.2731074845244450 ) ) ;
#101038=CARTESIAN_POINT ( 'NONE',  ( -16.93521499325732194, 66.00521388020870006, -149.1159989434308955 ) ) ;
#101050=LINE ( 'NONE', #202774, #55588 ) ;
#101086=ORIENTED_EDGE ( 'NONE', *, *, #246036, .F. ) ;
#101188=ORIENTED_EDGE ( 'NONE', *, *, #26632, .T. ) ;
#101255=CARTESIAN_POINT ( 'NONE',  ( -17.22361732159831149, 65.65484434140982728, -147.8938920103915962 ) ) ;
#101631=VECTOR ( 'NONE', #215186, 1000.000000000000000 ) ;
#101990=( BOUNDED_SURFACE ( )  B_SPLINE_SURFACE ( 3, 2, ( 
 ( #225374, #46743, #27230 ),
 ( #184986, #50586, #106709 ),
 ( #248821, #190130, #11498 ),
 ( #65030, #169315, #149736 ) ),
 .UNSPECIFIED., .F., .F., .T. ) 
 B_SPLINE_SURFACE_WITH_KNOTS ( ( 4, 4 ),
 ( 3, 3 ),
 ( 4.712388980384689674, 5.765869716888531116 ),
 ( 0.000000000000000000, 1.000000000000000000 ),
 .UNSPECIFIED. ) 
 GEOMETRIC_REPRESENTATION_ITEM ( )  RATIONAL_B_SPLINE_SURFACE ( (
 ( 1.000000000000000000, 0.7071067811865475727, 1.000000000000000000),
 ( 1.000000000000000000, 0.7953136715913589061, 1.000000000000000000),
 ( 1.000000000000000000, 0.8646876308614964701, 1.000000000000000000),
 ( 1.000000000000000000, 0.8984936768950676500, 1.000000000000000000) ) ) 
 REPRESENTATION_ITEM ( '' )  SURFACE ( )  );
#102009=ORIENTED_EDGE ( 'NONE', *, *, #60183, .F. ) ;
#102148=CARTESIAN_POINT ( 'NONE',  ( -16.93230518875208190, 65.99924963859245963, -157.4473291364229226 ) ) ;
#102196=DIRECTION ( 'NONE',  ( -1.073024830501117725E-15, 6.982962677686266711E-15, -1.000000000000000000 ) ) ;
#102228=CARTESIAN_POINT ( 'NONE',  ( -12.48127053791145435, 66.62341902196833132, -152.3961612375125014 ) ) ;
#102343=CARTESIAN_POINT ( 'NONE',  ( -16.93353400591626112, 65.99538760383930480, -149.0904230143190148 ) ) ;
#102453=EDGE_CURVE ( 'NONE', #46648, #56214, #25079, .T. ) ;
#102469=ORIENTED_EDGE ( 'NONE', *, *, #127329, .T. ) ;
#102555=CARTESIAN_POINT ( 'NONE',  ( -17.71734398241073549, 65.15764277154767115, -146.7979692315188345 ) ) ;
#102726=DIRECTION ( 'NONE',  ( 1.186688945009009831E-16, 1.000000000000000000, 6.982962677686266711E-15 ) ) ;
#102771=CARTESIAN_POINT ( 'NONE',  ( -16.88460203013674388, 66.04524099677652771, -149.1572156749861904 ) ) ;
#102806=CARTESIAN_POINT ( 'NONE',  ( -16.93658623642909689, 66.01961832835519317, -157.4112047553951754 ) ) ;
#102914=AXIS2_PLACEMENT_3D ( 'NONE', #79353, #21982, #141904 ) ;
#103081=VERTEX_POINT ( 'NONE', #246359 ) ;
#103445=CARTESIAN_POINT ( 'NONE',  ( -16.93262454970420094, 65.99797953208192780, -157.4501837107617348 ) ) ;
#103495=CARTESIAN_POINT ( 'NONE',  ( 18.39999999999999503, 70.35000000001224407, -149.1731074845243938 ) ) ;
#103537=CARTESIAN_POINT ( 'NONE',  ( -14.87770893841225295, 66.56936289831551790, -151.7548468664634811 ) ) ;
#103907=CARTESIAN_POINT ( 'NONE',  ( -16.85697194749129935, 66.09145628588862564, -157.0881032169105822 ) ) ;
#103969=CARTESIAN_POINT ( 'NONE',  ( -14.00000000000000178, 66.15000000001228386, -153.2731074845244166 ) ) ;
#103976=CARTESIAN_POINT ( 'NONE',  ( -14.45443560709638220, 66.54940788787860129, -154.9669191657160354 ) ) ;
#103986=ORIENTED_EDGE ( 'NONE', *, *, #208341, .T. ) ;
#104303=CARTESIAN_POINT ( 'NONE',  ( -18.40000000000000213, 70.35000000001224407, -149.1731074845243938 ) ) ;
#104348=LINE ( 'NONE', #203480, #90343 ) ;
#104582=ADVANCED_FACE ( 'NONE', ( #111424 ), #171436, .F. ) ;
#105007=ADVANCED_FACE ( 'NONE', ( #194528 ), #38025, .T. ) ;
#105219=CARTESIAN_POINT ( 'NONE',  ( 21.13736287352038445, 67.95335762362823573, -149.1731074845244223 ) ) ;
#105243=CARTESIAN_POINT ( 'NONE',  ( -15.70407651835961360, 66.64419340838212236, -153.7320049529782864 ) ) ;
#105637=VERTEX_POINT ( 'NONE', #175314 ) ;
#105648=ORIENTED_EDGE ( 'NONE', *, *, #154816, .F. ) ;
#105835=CARTESIAN_POINT ( 'NONE',  ( -16.81930730667007268, 66.06300193113824548, -157.2963397539862171 ) ) ;
#106379=FACE_OUTER_BOUND ( 'NONE', #244623, .T. ) ;
#106604=CARTESIAN_POINT ( 'NONE',  ( -16.87331047859649757, 66.05000000001224691, -149.1731074845244223 ) ) ;
#106689=CARTESIAN_POINT ( 'NONE',  ( -15.55912972643740488, 67.50912972644967169, -149.1731074845244223 ) ) ;
#106709=CARTESIAN_POINT ( 'NONE',  ( -17.04295772865478398, 65.97510057475076906, -157.3731074845244109 ) ) ;
#106747=B_SPLINE_CURVE_WITH_KNOTS ( 'NONE', 3,
 ( #77031, #196974, #40525, #37938, #35388, #61, #216547 ),
 .UNSPECIFIED., .F., .F.,
 ( 4, 3, 4 ),
 ( 3.469446951953614189E-18, 3.882884552234413058E-05, 5.798605692158380332E-05 ),
 .UNSPECIFIED. ) ;
#106799=DIRECTION ( 'NONE',  ( 0.000000000000000000, 1.000000000000000000, 6.982962677686266711E-15 ) ) ;
#107144=DIRECTION ( 'NONE',  ( -0.000000000000000000, -6.982962677686266711E-15, 1.000000000000000000 ) ) ;
#107287=VERTEX_POINT ( 'NONE', #204839 ) ;
#107575=EDGE_CURVE ( 'NONE', #227999, #62835, #216893, .T. ) ;
#107746=LINE ( 'NONE', #67341, #92307 ) ;
#107842=DIRECTION ( 'NONE',  ( 0.000000000000000000, -6.789366196018718420E-15, 1.000000000000000000 ) ) ;
#107926=EDGE_CURVE ( 'NONE', #201378, #105637, #194214, .T. ) ;
#108051=EDGE_CURVE ( 'NONE', #246673, #191026, #29432, .T. ) ;
#108129=EDGE_LOOP ( 'NONE', ( #228440, #240655, #245763 ) ) ;
#108426=CARTESIAN_POINT ( 'NONE',  ( -18.34374000495060386, 64.52683809664983983, -160.7731074845244450 ) ) ;
#108427=CARTESIAN_POINT ( 'NONE',  ( 13.54577453029516398, 66.54939790392371890, -151.5792115214277942 ) ) ;
#108462=DIRECTION ( 'NONE',  ( -1.000000000000000000, 0.000000000000000000, 0.000000000000000000 ) ) ;
#108569=CARTESIAN_POINT ( 'NONE',  ( -16.87383368123029825, 66.05000000001230376, -157.3731074845244393 ) ) ;
#108716=VECTOR ( 'NONE', #38970, 1000.000000000000000 ) ;
#108807=ORIENTED_EDGE ( 'NONE', *, *, #32043, .F. ) ;
#109056=CARTESIAN_POINT ( 'NONE',  ( -18.40000000000000213, 64.52683809664972614, -145.8490535513323891 ) ) ;
#109059=CARTESIAN_POINT ( 'NONE',  ( -16.82055514392384410, 66.05000000001228955, -157.3463094099821546 ) ) ;
#109106=CARTESIAN_POINT ( 'NONE',  ( -18.40000000000000213, 64.52683809664974035, -149.0731074845244279 ) ) ;
#109240=CARTESIAN_POINT ( 'NONE',  ( -16.87683809663752399, 66.15000000001225544, -149.9254715027207396 ) ) ;
#109433=ORIENTED_EDGE ( 'NONE', *, *, #176292, .T. ) ;
#109494=CARTESIAN_POINT ( 'NONE',  ( -16.92973740335358457, 66.00749618554368681, -149.1170484493211177 ) ) ;
#109716=DIRECTION ( 'NONE',  ( -1.073024830501117725E-15, 6.982962677686266711E-15, -1.000000000000000000 ) ) ;
#109720=CARTESIAN_POINT ( 'NONE',  ( 18.39999999999999503, 64.25000000001222134, -145.7731074845244450 ) ) ;
#109835=CARTESIAN_POINT ( 'NONE',  ( -16.88560720703333473, 66.04943515626260364, -157.3749955636607183 ) ) ;
#109918=ORIENTED_EDGE ( 'NONE', *, *, #222171, .F. ) ;
#109986=DIRECTION ( 'NONE',  ( -1.652117596168391700E-15, 1.000000000000000000, 6.982962677686266711E-15 ) ) ;
#110320=CARTESIAN_POINT ( 'NONE',  ( -18.40000000000000213, 64.25000000001230660, -157.3731074845244393 ) ) ;
#110323=ORIENTED_EDGE ( 'NONE', *, *, #58026, .T. ) ;
#110324=DIRECTION ( 'NONE',  ( -1.000000000000000000, -0.000000000000000000, -0.000000000000000000 ) ) ;
#110375=ORIENTED_EDGE ( 'NONE', *, *, #99174, .F. ) ;
#110720=ORIENTED_EDGE ( 'NONE', *, *, #211524, .T. ) ;
#110883=LINE ( 'NONE', #250392, #3850 ) ;
#110980=CARTESIAN_POINT ( 'NONE',  ( -16.79270642812263858, 66.05375578307364037, -149.1841742059602041 ) ) ;
#111007=CARTESIAN_POINT ( 'NONE',  ( -23.25000000000000355, 70.35000000001230092, -157.3731074845244109 ) ) ;
#111009=CARTESIAN_POINT ( 'NONE',  ( 15.74999999999999645, 66.65000000001228386, -153.2731074845244166 ) ) ;
#111194=EDGE_LOOP ( 'NONE', ( #159772, #211379, #6481, #230151, #3002 ) ) ;
#111424=FACE_OUTER_BOUND ( 'NONE', #42845, .T. ) ;
#111575=VECTOR ( 'NONE', #147908, 1000.000000000000000 ) ;
#111640=CARTESIAN_POINT ( 'NONE',  ( -16.77902162784673479, 66.05358074280444214, -157.3611162404550896 ) ) ;
#111853=VERTEX_POINT ( 'NONE', #21400 ) ;
#111917=VECTOR ( 'NONE', #129678, 1000.000000000000000 ) ;
#111989=ORIENTED_EDGE ( 'NONE', *, *, #195657, .F. ) ;
#112094=EDGE_CURVE ( 'NONE', #251500, #238447, #79736, .T. ) ;
#112366=ORIENTED_EDGE ( 'NONE', *, *, #25986, .F. ) ;
#112435=CARTESIAN_POINT ( 'NONE',  ( -16.88219499860498374, 66.04979357458471156, -157.3737977944171291 ) ) ;
#112439=EDGE_CURVE ( 'NONE', #164969, #17339, #213832, .T. ) ;
#112497=EDGE_LOOP ( 'NONE', ( #93954, #25957 ) ) ;
#113545=CARTESIAN_POINT ( 'NONE',  ( -16.89155683852755274, 66.05000000001493277, -149.8004793340643346 ) ) ;
#114054=FILL_AREA_STYLE ('',( #254806 ) ) ;
#114111=DIRECTION ( 'NONE',  ( 1.000000000000000000, 0.000000000000000000, 0.000000000000000000 ) ) ;
#114208=CARTESIAN_POINT ( 'NONE',  ( -16.81095280782811230, 66.05000000001230376, -157.3731074845252920 ) ) ;
#114211=VERTEX_POINT ( 'NONE', #129847 ) ;
#114222=CARTESIAN_POINT ( 'NONE',  ( -18.40000000000000213, 64.52683809664981140, -157.4731074845244621 ) ) ;
#114259=EDGE_LOOP ( 'NONE', ( #173077, #110323, #17950, #102469, #130613, #127287, #123786, #64939, #161193, #190387, #244631, #229690, #228044, #224550, #166127, #152494, #892, #221736 ) ) ;
#114273=ORIENTED_EDGE ( 'NONE', *, *, #176606, .F. ) ;
#114578=B_SPLINE_CURVE_WITH_KNOTS ( 'NONE', 3,
 ( #210742, #114208, #249868, #90776, #192466, #229033, #169089, #93353, #111640, #232900, #54222, #133765, #213296 ),
 .UNSPECIFIED., .F., .F.,
 ( 4, 3, 3, 3, 4 ),
 ( 1.075528555105620399E-16, 1.946463881814325270E-05, 3.922356109943460204E-05, 4.215060953239334383E-05, 4.415117091092807429E-05 ),
 .UNSPECIFIED. ) ;
#114662=ORIENTED_EDGE ( 'NONE', *, *, #71559, .F. ) ;
#114741=EDGE_CURVE ( 'NONE', #24761, #227999, #58733, .T. ) ;
#114780=AXIS2_PLACEMENT_3D ( 'NONE', #44394, #198634, #194815 ) ;
#114827=CARTESIAN_POINT ( 'NONE',  ( -16.82055514392372686, 66.05000000001226113, -149.1999055590666217 ) ) ;
#114906=FACE_OUTER_BOUND ( 'NONE', #54141, .T. ) ;
#115170=EDGE_CURVE ( 'NONE', #90118, #240031, #166716, .T. ) ;
#115392=PRODUCT_DEFINITION_FORMATION_WITH_SPECIFIED_SOURCE ( 'ANY', '', #72353, .NOT_KNOWN. ) ;
#115525=CIRCLE ( 'NONE', #78115, 0.5000000000000004441 ) ;
#115626=CARTESIAN_POINT ( 'NONE',  ( -16.87036670365549895, 66.01058118071065905, -157.5026676018264880 ) ) ;
#115796=EDGE_CURVE ( 'NONE', #32558, #252649, #121383, .T. ) ;
#115844=DIRECTION ( 'NONE',  ( 1.073024830501117725E-15, 6.982962677686266711E-15, -1.000000000000000000 ) ) ;
#116127=CARTESIAN_POINT ( 'NONE',  ( 16.87683809663749557, 66.05000000001226113, -149.1731074845244223 ) ) ;
#116185=CARTESIAN_POINT ( 'NONE',  ( 13.22261339317535445, 66.56344716000785411, -154.8451520117640996 ) ) ;
#116518=AXIS2_PLACEMENT_3D ( 'NONE', #232128, #32674, #33961 ) ;
#116599=CARTESIAN_POINT ( 'NONE',  ( -16.87036670365549895, 66.01058118071064484, -157.5026676018264595 ) ) ;
#116674=VECTOR ( 'NONE', #207193, 1000.000000000000000 ) ;
#116797=ORIENTED_EDGE ( 'NONE', *, *, #230436, .T. ) ;
#117165=CARTESIAN_POINT ( 'NONE',  ( -16.87368910959167678, 66.03872618332088962, -157.4106143878838395 ) ) ;
#117286=DIRECTION ( 'NONE',  ( 1.020425574104004196E-15, 6.982962677686266711E-15, -1.000000000000000000 ) ) ;
#117305=CARTESIAN_POINT ( 'NONE',  ( -20.65000000000000568, 68.75000000001232081, -157.3731074845244109 ) ) ;
#117642=EDGE_CURVE ( 'NONE', #68090, #22326, #60051, .T. ) ;
#117995=CARTESIAN_POINT ( 'NONE',  ( -18.38639463286148867, 64.51980042617634581, -160.7731074845244450 ) ) ;
#118238=CARTESIAN_POINT ( 'NONE',  ( -18.40000000000000213, 64.51332499825466016, -160.7731074845244450 ) ) ;
#118362=CARTESIAN_POINT ( 'NONE',  ( -23.25000000000000355, 70.35000000001232934, -160.7731074845243882 ) ) ;
#118444=LINE ( 'NONE', #61012, #39376 ) ;
#118455=B_SPLINE_CURVE_WITH_KNOTS ( 'NONE', 3,
 ( #82583, #145145, #203845, #5623, #42222, #22675, #202571, #61774, #222102, #167324, #25236, #102148, #103445, #183023, #43504, #63046, #164733, #224685, #46054 ),
 .UNSPECIFIED., .F., .F.,
 ( 4, 3, 3, 3, 3, 3, 4 ),
 ( 0.0001624081864585794055, 0.0001685232196531677375, 0.0001764526673566770378, 0.0001916878551483278104, 0.0002009890782182702088, 0.0002238845907555191150, 0.0002283406619926350520 ),
 .UNSPECIFIED. ) ;
#118518=AXIS2_PLACEMENT_3D ( 'NONE', #147240, #89822, #11604 ) ;
#118751=CARTESIAN_POINT ( 'NONE',  ( 12.47034474403011650, 66.62446189796425244, -154.1532316035335555 ) ) ;
#119086=ADVANCED_FACE ( 'NONE', ( #200969 ), #100548, .F. ) ;
#119111=FACE_OUTER_BOUND ( 'NONE', #244150, .T. ) ;
#119115=ADVANCED_FACE ( 'NONE', ( #242652 ), #2751, .T. ) ;
#119396=DIRECTION ( 'NONE',  ( 1.186688945009010077E-16, 1.000000000000000000, 6.982962677686266711E-15 ) ) ;
#119788=CARTESIAN_POINT ( 'NONE',  ( 20.27550659511088682, 66.78395627750346364, -160.7731074845244166 ) ) ;
#119858=CARTESIAN_POINT ( 'NONE',  ( -16.91247567987038281, 66.04091731634304097, -157.3943830259870822 ) ) ;
#119937=AXIS2_PLACEMENT_3D ( 'NONE', #188662, #89552, #107842 ) ;
#120054=CARTESIAN_POINT ( 'NONE',  ( 20.27550659511089037, 66.78395627750340680, -149.1731074845244223 ) ) ;
#120061=VERTEX_POINT ( 'NONE', #189779 ) ;
#120127=B_SPLINE_CURVE_WITH_KNOTS ( 'NONE', 3,
 ( #158529, #238030, #124522, #99783, #102343, #25426, #1979, #239330, #140197, #4549, #41150, #101038, #81498, #44980, #142767, #123231 ),
 .UNSPECIFIED., .F., .F.,
 ( 4, 3, 3, 3, 3, 4 ),
 ( 0.000000000000000000, 1.810570668010599751E-05, 2.740575833570006129E-05, 4.256816319434536945E-05, 5.213463471025743496E-05, 6.641585710718904932E-05 ),
 .UNSPECIFIED. ) ;
#120292=DIRECTION ( 'NONE',  ( 1.000000000000000000, 0.000000000000000000, 0.000000000000000000 ) ) ;
#120326=CIRCLE ( 'NONE', #118518, 1.749999999999999778 ) ;
#120624=LINE ( 'NONE', #257481, #68521 ) ;
#120766=ADVANCED_FACE ( 'NONE', ( #152315 ), #246638, .T. ) ;
#121061=( BOUNDED_SURFACE ( )  B_SPLINE_SURFACE ( 3, 2, ( 
 ( #232788, #171543, #168987 ),
 ( #54119, #208093, #34587 ),
 ( #213189, #251027, #167688 ),
 ( #247185, #68568, #128535 ) ),
 .UNSPECIFIED., .F., .F., .F. ) 
 B_SPLINE_SURFACE_WITH_KNOTS ( ( 4, 4 ),
 ( 3, 3 ),
 ( 5.727910411845712702, 5.983100554402349225 ),
 ( 0.000000000000000000, 1.000000000000000000 ),
 .UNSPECIFIED. ) 
 GEOMETRIC_REPRESENTATION_ITEM ( )  RATIONAL_B_SPLINE_SURFACE ( (
 ( 1.000000000000000000, 0.8946697475932141597, 1.000000000000000000),
 ( 1.000000000000000000, 0.9035312726220726676, 1.000000000000000000),
 ( 1.000000000000000000, 0.9104333467450284045, 1.000000000000000000),
 ( 1.000000000000000000, 0.9152888060719485130, 1.000000000000000000) ) ) 
 REPRESENTATION_ITEM ( '' )  SURFACE ( )  );
#121162=EDGE_CURVE ( 'NONE', #166364, #232094, #213216, .T. ) ;
#121323=EDGE_CURVE ( 'NONE', #232013, #196307, #245403, .T. ) ;
#121383=LINE ( 'NONE', #58770, #155244 ) ;
#121448=CARTESIAN_POINT ( 'NONE',  ( -23.25000000000000355, 70.35000000001232934, -160.7731074845243882 ) ) ;
#121511=ORIENTED_EDGE ( 'NONE', *, *, #150017, .T. ) ;
#121562=ADVANCED_FACE ( 'NONE', ( #255861, #218041, #197214 ), #219339, .T. ) ;
#121944=ORIENTED_EDGE ( 'NONE', *, *, #73310, .F. ) ;
#122105=VERTEX_POINT ( 'NONE', #64191 ) ;
#122176=ORIENTED_EDGE ( 'NONE', *, *, #112094, .F. ) ;
#122264=EDGE_CURVE ( 'NONE', #111853, #103081, #189278, .T. ) ;
#122299=CARTESIAN_POINT ( 'NONE',  ( 23.24999999999999645, 64.25000000001233502, -160.7731074845244450 ) ) ;
#122348=VECTOR ( 'NONE', #199311, 1000.000000000000000 ) ;
#122456=CARTESIAN_POINT ( 'NONE',  ( 18.39999999999999503, 64.25000000001230660, -157.3731074845244393 ) ) ;
#122883=DIRECTION ( 'NONE',  ( -1.000000000000000000, 0.000000000000000000, -0.000000000000000000 ) ) ;
#123034=CARTESIAN_POINT ( 'NONE',  ( -16.94225986326249611, 66.05000000001228955, -157.0763881089165181 ) ) ;
#123231=CARTESIAN_POINT ( 'NONE',  ( -16.94445028196807002, 66.00793639031451221, -149.1304376629428816 ) ) ;
#123564=DIRECTION ( 'NONE',  ( 1.000000000000000000, 0.000000000000000000, 0.000000000000000000 ) ) ;
#123663=ORIENTED_EDGE ( 'NONE', *, *, #30014, .F. ) ;
#123786=ORIENTED_EDGE ( 'NONE', *, *, #157424, .T. ) ;
#123830=ORIENTED_EDGE ( 'NONE', *, *, #208566, .T. ) ;
#123994=DIRECTION ( 'NONE',  ( -0.000000000000000000, -6.982962677686266711E-15, 1.000000000000000000 ) ) ;
#124030=DIRECTION ( 'NONE',  ( 0.000000000000000000, 1.000000000000000000, 0.000000000000000000 ) ) ;
#124168=CARTESIAN_POINT ( 'NONE',  ( -17.78043020864321022, 65.14640788800653581, -146.8600583188042208 ) ) ;
#124291=CARTESIAN_POINT ( 'NONE',  ( -16.79363873026997922, 66.05114977059379555, -149.1769537030789650 ) ) ;
#124316=CARTESIAN_POINT ( 'NONE',  ( -16.97683809663752186, 66.05000000001230376, -156.6207434663279514 ) ) ;
#124365=DIRECTION ( 'NONE',  ( -0.7071067811865301422, 0.7071067811865648922, 0.000000000000000000 ) ) ;
#124368=CARTESIAN_POINT ( 'NONE',  ( -16.97048361161166952, 66.05000000001223270, -149.6642231400940091 ) ) ;
#124502=AXIS2_PLACEMENT_3D ( 'NONE', #88813, #168435, #69295 ) ;
#124522=CARTESIAN_POINT ( 'NONE',  ( -16.93589915522259304, 65.99137474131637759, -149.0825473825641154 ) ) ;
#124544=VERTEX_POINT ( 'NONE', #166284 ) ;
#124564=CARTESIAN_POINT ( 'NONE',  ( 20.09999999999999787, 66.25000000001227818, -157.3731074845244393 ) ) ;
#124792=CARTESIAN_POINT ( 'NONE',  ( -16.92280123533687686, 66.05000000001230376, -157.1724751704392986 ) ) ;
#124851=DIRECTION ( 'NONE',  ( 1.186688945009010077E-16, 1.000000000000000000, 6.982962677686266711E-15 ) ) ;
#125141=ORIENTED_EDGE ( 'NONE', *, *, #127329, .F. ) ;
#125293=DIRECTION ( 'NONE',  ( 1.000000000000000000, 0.000000000000000000, 0.000000000000000000 ) ) ;
#125675=CARTESIAN_POINT ( 'NONE',  ( -20.65000000000000568, 70.35000000001224407, -149.1731074845243938 ) ) ;
#125908=CARTESIAN_POINT ( 'NONE',  ( 18.39999999999999503, 64.25000000001230660, -157.3731074845244393 ) ) ;
#126341=DIRECTION ( 'NONE',  ( 0.000000000000000000, -1.000000000000000000, -6.982962677686266711E-15 ) ) ;
#126531=ADVANCED_FACE ( 'NONE', ( #234778 ), #53212, .F. ) ;
#126581=ORIENTED_EDGE ( 'NONE', *, *, #77361, .F. ) ;
#126595=EDGE_CURVE ( 'NONE', #127923, #4697, #79845, .T. ) ;
#126650=DIRECTION ( 'NONE',  ( -1.000000000000000000, 0.000000000000000000, 0.000000000000000000 ) ) ;
#126835=LINE ( 'NONE', #147686, #30662 ) ;
#126926=CARTESIAN_POINT ( 'NONE',  ( -15.55912972643740488, 67.50912972644967169, -149.0731074845244279 ) ) ;
#126944=CARTESIAN_POINT ( 'NONE',  ( -16.87331047859651179, 66.05000000001230376, -157.3731074845244393 ) ) ;
#127287=ORIENTED_EDGE ( 'NONE', *, *, #159450, .T. ) ;
#127326=( GEOMETRIC_REPRESENTATION_CONTEXT ( 3 ) GLOBAL_UNCERTAINTY_ASSIGNED_CONTEXT ( ( #162634 ) ) GLOBAL_UNIT_ASSIGNED_CONTEXT ( ( #72395, #235288, #55337 ) ) REPRESENTATION_CONTEXT ( 'NONE', 'WORKASPACE' ) );
#127329=EDGE_CURVE ( 'NONE', #230022, #201378, #114578, .T. ) ;
#127404=VERTEX_POINT ( 'NONE', #76345 ) ;
#127462=DIRECTION ( 'NONE',  ( 1.186688945009009831E-16, 1.000000000000000000, 6.982962677686266711E-15 ) ) ;
#127580=EDGE_CURVE ( 'NONE', #252649, #24761, #115525, .T. ) ;
#127694=DIRECTION ( 'NONE',  ( -1.000000000000000000, -7.125593699324843413E-30, 1.020425574104004196E-15 ) ) ;
#127923=VERTEX_POINT ( 'NONE', #251495 ) ;
#127941=FACE_OUTER_BOUND ( 'NONE', #65058, .T. ) ;
#128169=CARTESIAN_POINT ( 'NONE',  ( -16.97048326478264357, 66.05000000001231797, -156.8820006043973194 ) ) ;
#128197=VERTEX_POINT ( 'NONE', #165238 ) ;
#128202=ORIENTED_EDGE ( 'NONE', *, *, #65681, .T. ) ;
#128266=CARTESIAN_POINT ( 'NONE',  ( -15.15564720441980384, 66.58929125296516816, -151.9538990786803083 ) ) ;
#128535=CARTESIAN_POINT ( 'NONE',  ( -16.87036670365549540, 66.01058118071064484, -157.5026676018264880 ) ) ;
#128598=CARTESIAN_POINT ( 'NONE',  ( -15.75000000000000355, 66.65000000001228386, -153.2731074845243882 ) ) ;
#128713=CARTESIAN_POINT ( 'NONE',  ( -12.29659703204452015, 66.64411154550971617, -153.7344645877464302 ) ) ;
#128772=CARTESIAN_POINT ( 'NONE',  ( -16.89146115310546392, 66.04855675435578632, -149.1682850655701884 ) ) ;
#129031=EDGE_LOOP ( 'NONE', ( #38080, #103986 ) ) ;
#129110=CARTESIAN_POINT ( 'NONE',  ( -12.25000000000000178, 66.15000000001228386, -153.2731074845244166 ) ) ;
#129306=PLANE ( 'NONE',  #257031 ) ;
#129678=DIRECTION ( 'NONE',  ( 1.000000000000000000, -1.646408749285562060E-14, -1.073024830501232702E-15 ) ) ;
#129749=CARTESIAN_POINT ( 'NONE',  ( -17.01825945287482966, 65.95000000001232365, -157.3731074845244393 ) ) ;
#129847=CARTESIAN_POINT ( 'NONE',  ( -17.11825945287481332, 66.05000000001224691, -149.2731074845244450 ) ) ;
#129964=CARTESIAN_POINT ( 'NONE',  ( -12.47155713865592119, 66.62433047358651095, -154.1553174751385313 ) ) ;
#130169=DIRECTION ( 'NONE',  ( -1.000000000000000000, 1.646408749285563322E-14, -1.073024830501002749E-15 ) ) ;
#130313=ORIENTED_EDGE ( 'NONE', *, *, #235281, .T. ) ;
#130317=CYLINDRICAL_SURFACE ( 'NONE', #243778, 0.9000000000000014655 ) ;
#130534=CARTESIAN_POINT ( 'NONE',  ( -16.87333278164146577, 66.11739021543348827, -149.6562752906779110 ) ) ;
#130544=CARTESIAN_POINT ( 'NONE',  ( 12.25000000000000000, 66.65000000001228386, -153.2731074845244166 ) ) ;
#130593=ORIENTED_EDGE ( 'NONE', *, *, #126595, .T. ) ;
#130613=ORIENTED_EDGE ( 'NONE', *, *, #107926, .T. ) ;
#130944=ORIENTED_EDGE ( 'NONE', *, *, #114741, .T. ) ;
#131023=CARTESIAN_POINT ( 'NONE',  ( 12.25000000000000000, 66.65000000001228386, -153.2731074845244166 ) ) ;
#131178=ORIENTED_EDGE ( 'NONE', *, *, #180528, .F. ) ;
#131423=CARTESIAN_POINT ( 'NONE',  ( 15.39793903038208001, 66.61031399435661626, -154.3502639781730750 ) ) ;
#131532=CARTESIAN_POINT ( 'NONE',  ( 23.04999999999999716, 67.17743825834591576, -160.7731074845244166 ) ) ;
#131541=VECTOR ( 'NONE', #55151, 1000.000000000000000 ) ;
#131625=ORIENTED_EDGE ( 'NONE', *, *, #213297, .F. ) ;
#131820=CARTESIAN_POINT ( 'NONE',  ( -16.77431908686106965, 66.05419424549425855, -149.1872682668742129 ) ) ;
#131824=DIRECTION ( 'NONE',  ( 0.000000000000000000, -1.000000000000000000, -6.982962677686266711E-15 ) ) ;
#131832=CARTESIAN_POINT ( 'NONE',  ( 15.75000000000000000, 66.65000000001229807, -153.1573643172505683 ) ) ;
#131978=CARTESIAN_POINT ( 'NONE',  ( -33.72168855820451938, 66.05000000001223270, -149.1731074845243654 ) ) ;
#132062=CARTESIAN_POINT ( 'NONE',  ( -18.40000000000000568, 64.58541674041244107, -149.1731074845244507 ) ) ;
#132130=LINE ( 'NONE', #34342, #229421 ) ;
#132251=ORIENTED_EDGE ( 'NONE', *, *, #235445, .F. ) ;
#132264=CARTESIAN_POINT ( 'NONE',  ( -23.25000000000000355, 64.25000000001233502, -160.7731074845244450 ) ) ;
#132418=CARTESIAN_POINT ( 'NONE',  ( 21.72449340488910252, 65.71604372252116377, -157.3731074845244393 ) ) ;
#132626=CARTESIAN_POINT ( 'NONE',  ( -18.40000000000000213, 70.35000000001224407, -149.1731074845243938 ) ) ;
#132721=EDGE_CURVE ( 'NONE', #222558, #120061, #2931, .T. ) ;
#132750=ORIENTED_EDGE ( 'NONE', *, *, #194776, .F. ) ;
#132836=VERTEX_POINT ( 'NONE', #111007 ) ;
#133060=PRODUCT_CONTEXT ( 'NONE', #177321, 'mechanical' ) ;
#133087=ORIENTED_EDGE ( 'NONE', *, *, #52301, .F. ) ;
#133116=CARTESIAN_POINT ( 'NONE',  ( -16.97683809663752186, 66.05000000001224691, -149.9254715027207396 ) ) ;
#133125=CARTESIAN_POINT ( 'NONE',  ( 15.69410316191959254, 66.64325398293399871, -152.8197477631602226 ) ) ;
#133198=VERTEX_POINT ( 'NONE', #10332 ) ;
#133302=CARTESIAN_POINT ( 'NONE',  ( -16.87036670365548474, 66.01058118071060221, -149.0435473672224020 ) ) ;
#133716=CARTESIAN_POINT ( 'NONE',  ( -21.65000000000000213, 68.75000000001232081, -157.3731074845244109 ) ) ;
#133765=CARTESIAN_POINT ( 'NONE',  ( -16.77732147278574715, 66.05403306743885139, -157.3595987276486312 ) ) ;
#134062=PRODUCT_DEFINITION_CONTEXT ( 'detailed design', #192501, 'design' ) ;
#134337=ORIENTED_EDGE ( 'NONE', *, *, #28131, .T. ) ;
#134364=CARTESIAN_POINT ( 'NONE',  ( -18.39999999999999858, 64.52683809664983983, -160.6971614177164724 ) ) ;
#134369=CARTESIAN_POINT ( 'NONE',  ( -16.82542659449977762, 66.06550010858478572, -149.2677430845504318 ) ) ;
#134461=ORIENTED_EDGE ( 'NONE', *, *, #135624, .T. ) ;
#134532=CARTESIAN_POINT ( 'NONE',  ( -16.77683809663752257, 66.05416425680809311, -149.1870565036286109 ) ) ;
#134582=EDGE_CURVE ( 'NONE', #22326, #161169, #152109, .T. ) ;
#134684=CARTESIAN_POINT ( 'NONE',  ( -16.98495255085916611, 65.99443563401746360, -149.1577246907449137 ) ) ;
#135160=DIRECTION ( 'NONE',  ( 0.000000000000000000, 0.000000000000000000, 1.000000000000000000 ) ) ;
#135516=CARTESIAN_POINT ( 'NONE',  ( 12.25000000000000000, 66.15000000001228386, -153.2731074845244450 ) ) ;
#135624=EDGE_CURVE ( 'NONE', #107287, #227999, #73292, .T. ) ;
#135632=CARTESIAN_POINT ( 'NONE',  ( -17.78241384945712156, 65.14442424720434133, -146.7721451569937585 ) ) ;
#135658=CARTESIAN_POINT ( 'NONE',  ( -16.88783316861802319, 66.05000000001224691, -149.2753715265037044 ) ) ;
#135795=DIRECTION ( 'NONE',  ( -0.000000000000000000, -6.982962677686266711E-15, 1.000000000000000000 ) ) ;
#135822=CARTESIAN_POINT ( 'NONE',  ( -16.87683809663752399, 66.15000000001225544, -149.9254715027207396 ) ) ;
#135970=CARTESIAN_POINT ( 'NONE',  ( -16.94445028196807002, 66.00793639031451221, -149.1304376629428816 ) ) ;
#136162=SURFACE_SIDE_STYLE ('',( #56621 ) ) ;
#136434=ORIENTED_EDGE ( 'NONE', *, *, #246684, .T. ) ;
#136441=PLANE ( 'NONE',  #80303 ) ;
#136549=CARTESIAN_POINT ( 'NONE',  ( -16.97092634996628036, 65.99911103366434872, -149.1532502508223672 ) ) ;
#136755=CARTESIAN_POINT ( 'NONE',  ( -18.40000000000000213, 70.35000000001230092, -157.3731074845244109 ) ) ;
#136971=PLANE ( 'NONE',  #39893 ) ;
#136984=CIRCLE ( 'NONE', #32986, 1.500000000000001332 ) ;
#137010=CARTESIAN_POINT ( 'NONE',  ( 14.11444803880197441, 66.54256847116334939, -155.0231905466248179 ) ) ;
#137425=CARTESIAN_POINT ( 'NONE',  ( -16.85718274719460652, 66.02385768539041067, -157.4597611523423666 ) ) ;
#137719=FACE_OUTER_BOUND ( 'NONE', #237039, .T. ) ;
#138071=( GEOMETRIC_REPRESENTATION_CONTEXT ( 3 ) GLOBAL_UNCERTAINTY_ASSIGNED_CONTEXT ( ( #206886 ) ) GLOBAL_UNIT_ASSIGNED_CONTEXT ( ( #169016, #12489, #24680 ) ) REPRESENTATION_CONTEXT ( 'NONE', 'WORKASPACE' ) );
#138273=CARTESIAN_POINT ( 'NONE',  ( 12.25000000000000000, 66.65000000001228386, -153.5015881126993520 ) ) ;
#138353=CARTESIAN_POINT ( 'NONE',  ( 20.04999999999999716, 67.25000000001230660, -160.7731074845244166 ) ) ;
#138409=LINE ( 'NONE', #100560, #1929 ) ;
#138470=EDGE_LOOP ( 'NONE', ( #246384, #60022, #165310, #140152 ) ) ;
#138551=CARTESIAN_POINT ( 'NONE',  ( -21.65000000000000213, 68.75000000001226397, -149.1731074845244223 ) ) ;
#138913=ADVANCED_FACE ( 'NONE', ( #149582 ), #64876, .T. ) ;
#139225=DIRECTION ( 'NONE',  ( 0.000000000000000000, 6.982962677686266711E-15, -1.000000000000000000 ) ) ;
#139369=CARTESIAN_POINT ( 'NONE',  ( -16.94275863009466576, 66.01050395134991788, -157.4148048665655608 ) ) ;
#139384=VERTEX_POINT ( 'NONE', #124564 ) ;
#139442=DIRECTION ( 'NONE',  ( 0.000000000000000000, 1.000000000000000000, 6.982962677686266711E-15 ) ) ;
#139477=ORIENTED_EDGE ( 'NONE', *, *, #83834, .T. ) ;
#139704=DIRECTION ( 'NONE',  ( 1.000000000000000000, 0.000000000000000000, 0.000000000000000000 ) ) ;
#139846=B_SPLINE_CURVE_WITH_KNOTS ( 'NONE', 3,
 ( #94568, #117995, #78845, #194988, #95842, #237936, #59255 ),
 .UNSPECIFIED., .F., .F.,
 ( 4, 3, 4 ),
 ( 0.000000000000000000, 4.520325912680430423E-05, 5.794988040901246848E-05 ),
 .UNSPECIFIED. ) ;
#139954=AXIS2_PLACEMENT_3D ( 'NONE', #63628, #143147, #184853 ) ;
#139963=CARTESIAN_POINT ( 'NONE',  ( -16.78270389226384651, 66.05262738339523310, -149.1819004476129464 ) ) ;
#140092=CARTESIAN_POINT ( 'NONE',  ( -12.68215100488890634, 66.60336962369453317, -152.1160500917060858 ) ) ;
#140115=DIRECTION ( 'NONE',  ( 1.000000000000000000, 0.000000000000000000, 0.000000000000000000 ) ) ;
#140152=ORIENTED_EDGE ( 'NONE', *, *, #186062, .F. ) ;
#140197=CARTESIAN_POINT ( 'NONE',  ( -16.93234230245722216, 66.00189262946514646, -149.1054172028581775 ) ) ;
#140294=ORIENTED_EDGE ( 'NONE', *, *, #25046, .T. ) ;
#140299=DIRECTION ( 'NONE',  ( 1.000000000000000000, 0.000000000000000000, 0.000000000000000000 ) ) ;
#140334=VECTOR ( 'NONE', #247739, 1000.000000000000000 ) ;
#140479=CARTESIAN_POINT ( 'NONE',  ( -16.89935556175678855, 66.05000000001231797, -156.8834311216385515 ) ) ;
#140546=DIRECTION ( 'NONE',  ( -0.000000000000000000, -6.982962677686266711E-15, 1.000000000000000000 ) ) ;
#140583=ORIENTED_EDGE ( 'NONE', *, *, #21238, .F. ) ;
#140636=CARTESIAN_POINT ( 'NONE',  ( -16.86379686415369150, 66.02478224075908031, -149.0897175954341662 ) ) ;
#140745=FILL_AREA_STYLE ('',( #181174 ) ) ;
#140782=DIRECTION ( 'NONE',  ( 1.652117596168391700E-15, -1.000000000000000000, -6.982962677686266711E-15 ) ) ;
#140789=ORIENTED_EDGE ( 'NONE', *, *, #52352, .F. ) ;
#140836=VECTOR ( 'NONE', #159383, 1000.000000000000000 ) ;
#141147=B_SPLINE_CURVE_WITH_KNOTS ( 'NONE', 3,
 ( #44752, #203810, #459, #99545, #139963, #179149, #124291, #159562, #25200, #78709 ),
 .UNSPECIFIED., .F., .F.,
 ( 4, 3, 3, 4 ),
 ( -2.000561356218653466E-06, 0.000000000000000000, 1.787822682428266431E-05, 4.206475347089715442E-05 ),
 .UNSPECIFIED. ) ;
#141357=PLANE ( 'NONE',  #174633 ) ;
#141390=CARTESIAN_POINT ( 'NONE',  ( -12.25000000000000000, 66.65000000001226965, -153.1573643172505115 ) ) ;
#141811=LINE ( 'NONE', #2287, #75750 ) ;
#141904=DIRECTION ( 'NONE',  ( -1.000000000000000000, 7.492892343619937423E-30, -1.073024830501117725E-15 ) ) ;
#141952=CARTESIAN_POINT ( 'NONE',  ( -16.94333152886235183, 66.00965798856181266, -157.4151390155788590 ) ) ;
#141992=VECTOR ( 'NONE', #122883, 1000.000000000000000 ) ;
#142107=EDGE_CURVE ( 'NONE', #215608, #103081, #213382, .T. ) ;
#142206=ORIENTED_EDGE ( 'NONE', *, *, #54345, .T. ) ;
#142449=EDGE_CURVE ( 'NONE', #14807, #167594, #104348, .T. ) ;
#142490=VECTOR ( 'NONE', #242616, 1000.000000000000000 ) ;
#142659=CARTESIAN_POINT ( 'NONE',  ( -14.45422546970482891, 66.54939790392373311, -151.5792115214277374 ) ) ;
#142767=CARTESIAN_POINT ( 'NONE',  ( -16.94132844910799918, 66.00756324483191406, -149.1269057285421411 ) ) ;
#142787=LINE ( 'NONE', #238054, #85283 ) ;
#143112=CARTESIAN_POINT ( 'NONE',  ( -14.56556274378147897, 66.55344247693973614, -154.9331655301785133 ) ) ;
#143147=DIRECTION ( 'NONE',  ( 1.000000000000000000, -1.186688945009010077E-16, -8.286604613020808509E-31 ) ) ;
#143435=LINE ( 'NONE', #222965, #9927 ) ;
#143616=CARTESIAN_POINT ( 'NONE',  ( 20.73486653747088582, 68.75000000001222134, -149.1731074845244223 ) ) ;
#144216=CARTESIAN_POINT ( 'NONE',  ( -16.89268316805466341, 66.04827818677011919, -157.3788599630699707 ) ) ;
#144326=ORIENTED_EDGE ( 'NONE', *, *, #234756, .F. ) ;
#144895=LINE ( 'NONE', #219307, #234488 ) ;
#144988=CARTESIAN_POINT ( 'NONE',  ( 20.73486653747088937, 68.25000000001222134, -149.1731074845244223 ) ) ;
#145145=CARTESIAN_POINT ( 'NONE',  ( -16.94309007106720699, 66.00777380744230527, -157.4173162019689016 ) ) ;
#145364=VECTOR ( 'NONE', #214768, 999.9999999999998863 ) ;
#145719=PLANE ( 'NONE',  #139954 ) ;
#145744=ORIENTED_EDGE ( 'NONE', *, *, #222939, .F. ) ;
#145806=ORIENTED_EDGE ( 'NONE', *, *, #151671, .F. ) ;
#146128=CARTESIAN_POINT ( 'NONE',  ( -16.94445028196808778, 66.00793639031455484, -157.4157773061059800 ) ) ;
#146291=VECTOR ( 'NONE', #59609, 1000.000000000000000 ) ;
#146632=VECTOR ( 'NONE', #56739, 1000.000000000000000 ) ;
#146856=CARTESIAN_POINT ( 'NONE',  ( -17.11825945287482753, 66.05000000001230376, -157.2731074845244166 ) ) ;
#146964=CARTESIAN_POINT ( 'NONE',  ( -13.12432614554023935, 66.56923500458995591, -154.7925700897739887 ) ) ;
#147189=PLANE ( 'NONE',  #227977 ) ;
#147240=CARTESIAN_POINT ( 'NONE',  ( -14.00000000000000178, 66.15000000001228386, -153.2731074845244166 ) ) ;
#147686=CARTESIAN_POINT ( 'NONE',  ( 18.39999999999999503, 70.35000000001224407, -149.1731074845243938 ) ) ;
#147892=ORIENTED_EDGE ( 'NONE', *, *, #209466, .T. ) ;
#147908=DIRECTION ( 'NONE',  ( 1.000000000000000000, 0.000000000000000000, 0.000000000000000000 ) ) ;
#147998=ORIENTED_EDGE ( 'NONE', *, *, #192474, .T. ) ;
#148070=EDGE_CURVE ( 'NONE', #120061, #151479, #120127, .T. ) ;
#148188=ORIENTED_EDGE ( 'NONE', *, *, #234756, .T. ) ;
#148313=DIRECTION ( 'NONE',  ( 1.000000000000000000, -1.186688945009009831E-16, -8.286604613020806758E-31 ) ) ;
#148653=FACE_OUTER_BOUND ( 'NONE', #192056, .T. ) ;
#148677=ADVANCED_FACE ( 'NONE', ( #182282 ), #2329, .F. ) ;
#148870=CARTESIAN_POINT ( 'NONE',  ( 20.27550659511088682, 66.78395627750344943, -157.3731074845244393 ) ) ;
#148885=DIRECTION ( 'NONE',  ( -1.073024830501117725E-15, -6.982962677686266711E-15, 1.000000000000000000 ) ) ;
#149126=CARTESIAN_POINT ( 'NONE',  ( -15.75000000000000355, 66.65000000001228386, -153.2731074845243882 ) ) ;
#149516=DIRECTION ( 'NONE',  ( 0.000000000000000000, 0.000000000000000000, -1.000000000000000000 ) ) ;
#149582=FACE_OUTER_BOUND ( 'NONE', #138470, .T. ) ;
#149736=CARTESIAN_POINT ( 'NONE',  ( -16.93388492042258164, 66.01145817749640798, -157.4236526077106078 ) ) ;
#149942=CARTESIAN_POINT ( 'NONE',  ( 18.54999999999999716, 66.05000000001228955, -157.3731074845244962 ) ) ;
#149961=ORIENTED_EDGE ( 'NONE', *, *, #156602, .F. ) ;
#150017=EDGE_CURVE ( 'NONE', #166364, #220255, #88640, .T. ) ;
#150079=CARTESIAN_POINT ( 'NONE',  ( -20.65000000000000568, 68.75000000001232081, -157.3731074845244109 ) ) ;
#150089=CARTESIAN_POINT ( 'NONE',  ( 20.99999999999999645, 66.25000000001233502, -160.7731074845244166 ) ) ;
#150138=CARTESIAN_POINT ( 'NONE',  ( 14.88075390448864255, 66.56831044948815190, -151.7438174522883685 ) ) ;
#150156=ORIENTED_EDGE ( 'NONE', *, *, #230819, .T. ) ;
#150199=ADVANCED_FACE ( 'NONE', ( #59779 ), #38980, .F. ) ;
#150277=CARTESIAN_POINT ( 'NONE',  ( -16.89060415895971090, 66.04877923721008415, -157.3771872602539474 ) ) ;
#150355=CARTESIAN_POINT ( 'NONE',  ( -18.40000000000000213, 64.66825945288707089, -149.1731074845244507 ) ) ;
#150446=ORIENTED_EDGE ( 'NONE', *, *, #25477, .F. ) ;
#150549=ORIENTED_EDGE ( 'NONE', *, *, #52352, .T. ) ;
#150742=LINE ( 'NONE', #231571, #81152 ) ;
#151002=CARTESIAN_POINT ( 'NONE',  ( 15.06592377766031987, 66.58221053306006354, -154.6657229405476244 ) ) ;
#151106=VECTOR ( 'NONE', #215725, 1000.000000000000000 ) ;
#151268=ADVANCED_FACE ( 'NONE', ( #39124 ), #58640, .F. ) ;
#151392=ORIENTED_EDGE ( 'NONE', *, *, #112439, .T. ) ;
#151418=CARTESIAN_POINT ( 'NONE',  ( 12.25000000000000355, 66.65000000001226965, -153.1588398769083028 ) ) ;
#151479=VERTEX_POINT ( 'NONE', #53222 ) ;
#151632=VERTEX_POINT ( 'NONE', #34985 ) ;
#151671=EDGE_CURVE ( 'NONE', #230269, #47244, #136984, .T. ) ;
#151908=ORIENTED_EDGE ( 'NONE', *, *, #80827, .F. ) ;
#152109=B_SPLINE_CURVE_WITH_KNOTS ( 'NONE', 3,
 ( #216240, #15516, #235811, #20643, #80562, #155030, #117165, #196681, #79291, #256607 ),
 .UNSPECIFIED., .F., .F.,
 ( 4, 3, 3, 4 ),
 ( 0.000000000000000000, 4.874959354404207151E-05, 9.785140065121151641E-05, 0.0001360444631936073986 ),
 .UNSPECIFIED. ) ;
#152246=ORIENTED_EDGE ( 'NONE', *, *, #54345, .F. ) ;
#152315=FACE_OUTER_BOUND ( 'NONE', #92274, .T. ) ;
#152483=MECHANICAL_DESIGN_GEOMETRIC_PRESENTATION_REPRESENTATION('',(#160686),#48212);
#152494=ORIENTED_EDGE ( 'NONE', *, *, #11081, .F. ) ;
#152605=CARTESIAN_POINT ( 'NONE',  ( -17.11825945287481332, 66.05000000001224691, -149.2731074845244450 ) ) ;
#152618=ADVANCED_FACE ( 'NONE', ( #222900 ), #43002, .F. ) ;
#152709=CARTESIAN_POINT ( 'NONE',  ( -16.85697194749129224, 66.09145628588855459, -149.4581117521382509 ) ) ;
#152870=CARTESIAN_POINT ( 'NONE',  ( -16.88815647973233780, 66.04916738069655935, -157.3758904211984202 ) ) ;
#152894=VERTEX_POINT ( 'NONE', #222575 ) ;
#153453=ADVANCED_FACE ( 'NONE', ( #154047 ), #233548, .F. ) ;
#153498=PLANE ( 'NONE',  #68453 ) ;
#153513=CARTESIAN_POINT ( 'NONE',  ( 0.000000000000000000, 0.000000000000000000, 0.000000000000000000 ) ) ;
#153622=CARTESIAN_POINT ( 'NONE',  ( -16.93388492042257454, 66.01145817749633693, -149.1225623613382538 ) ) ;
#153965=DIRECTION ( 'NONE',  ( 0.000000000000000000, -6.982962677686266711E-15, 1.000000000000000000 ) ) ;
#153977=CARTESIAN_POINT ( 'NONE',  ( -16.91256925476569606, 66.01426884188406063, -149.0554649955191735 ) ) ;
#153981=CARTESIAN_POINT ( 'NONE',  ( -18.40000000000000213, 64.25000000001222134, -145.7731074845244450 ) ) ;
#154013=ORIENTED_EDGE ( 'NONE', *, *, #96157, .T. ) ;
#154047=FACE_OUTER_BOUND ( 'NONE', #66846, .T. ) ;
#154167=ADVANCED_FACE ( 'NONE', ( #223907 ), #240932, .T. ) ;
#154214=DIRECTION ( 'NONE',  ( -0.000000000000000000, 6.982962677686266711E-15, -1.000000000000000000 ) ) ;
#154411=ORIENTED_EDGE ( 'NONE', *, *, #122264, .T. ) ;
#154816=EDGE_CURVE ( 'NONE', #77397, #251500, #65497, .T. ) ;
#154874=AXIS2_PLACEMENT_3D ( 'NONE', #188014, #115844, #57124 ) ;
#155030=CARTESIAN_POINT ( 'NONE',  ( -16.86757978335472075, 66.03434962097800565, -157.4251028313569236 ) ) ;
#155244=VECTOR ( 'NONE', #198301, 1000.000000000000000 ) ;
#155245=CARTESIAN_POINT ( 'NONE',  ( -16.94107738177413225, 65.98576071487563866, -149.0731074845244564 ) ) ;
#155269=B_SPLINE_CURVE_WITH_KNOTS ( 'NONE', 3,
 ( #135822, #34205, #237518, #198378, #177575, #255739, #257019, #77142, #78425, #236218, #54990, #57568, #19763, #134532 ),
 .UNSPECIFIED., .F., .F.,
 ( 4, 2, 2, 2, 2, 2, 4 ),
 ( 0.000000000000000000, 0.0003823333598417659224, 0.0005735000397626485854, 0.0006690833797230926003, 0.0007168750497033104336, 0.0007407708846934199466, 0.0007646667196835293511 ),
 .UNSPECIFIED. ) ;
#156359=ORIENTED_EDGE ( 'NONE', *, *, #27545, .T. ) ;
#156532=CARTESIAN_POINT ( 'NONE',  ( -17.73285935862685392, 65.14201819622533662, -146.7645456747499111 ) ) ;
#156602=EDGE_CURVE ( 'NONE', #127404, #167594, #13146, .T. ) ;
#156878=AXIS2_PLACEMENT_3D ( 'NONE', #236813, #77727, #41223 ) ;
#156890=VECTOR ( 'NONE', #30705, 1000.000000000000000 ) ;
#157157=EDGE_CURVE ( 'NONE', #257588, #230269, #239579, .T. ) ;
#157302=AXIS2_PLACEMENT_3D ( 'NONE', #58077, #197602, #171671 ) ;
#157337=DIRECTION ( 'NONE',  ( 1.000000000000000000, 0.000000000000000000, 0.000000000000000000 ) ) ;
#157352=ORIENTED_EDGE ( 'NONE', *, *, #68785, .T. ) ;
#157424=EDGE_CURVE ( 'NONE', #77397, #46041, #150742, .T. ) ;
#157523=EDGE_CURVE ( 'NONE', #103081, #127404, #120624, .T. ) ;
#157816=DIRECTION ( 'NONE',  ( 0.7071067811865487940, -0.7071067811865462405, -4.216150419019403701E-15 ) ) ;
#157853=CARTESIAN_POINT ( 'NONE',  ( 18.39999999999997371, 64.52683809664972614, -145.7731074845244450 ) ) ;
#157930=ORIENTED_EDGE ( 'NONE', *, *, #188627, .F. ) ;
#158315=EDGE_LOOP ( 'NONE', ( #29581, #202864, #24178, #19912, #109918, #76470, #154411, #30288, #246516 ) ) ;
#158319=( BOUNDED_CURVE ( )  B_SPLINE_CURVE ( 3, ( #9536, #248158, #132062, #150355 ),
 .UNSPECIFIED., .F., .F. ) 
 B_SPLINE_CURVE_WITH_KNOTS ( ( 4, 4 ),
 ( -9.769962616701377556E-15, 1.570796326794891673 ),
 .UNSPECIFIED. ) 
 CURVE ( )  GEOMETRIC_REPRESENTATION_ITEM ( )  RATIONAL_B_SPLINE_CURVE ( ( 1.000000000000000000, 0.8047378541243637162, 0.8047378541243637162, 1.000000000000000000 ) ) 
 REPRESENTATION_ITEM ( '' )  );
#158328=CARTESIAN_POINT ( 'NONE',  ( -16.91256925476572093, 66.01426884188410327, -157.4907499735297165 ) ) ;
#158429=CARTESIAN_POINT ( 'NONE',  ( -12.42749937872396870, 66.62931007840965947, -152.4966423578633794 ) ) ;
#158529=CARTESIAN_POINT ( 'NONE',  ( -16.94107738177414291, 65.98576071487562444, -149.0731074845244279 ) ) ;
#158738=ADVANCED_FACE ( 'NONE', ( #83152 ), #145719, .F. ) ;
#158761=CARTESIAN_POINT ( 'NONE',  ( 15.74999999999999645, 66.15000000001228386, -153.2731074845244450 ) ) ;
#158817=VERTEX_POINT ( 'NONE', #88295 ) ;
#158912=LINE ( 'NONE', #59755, #59846 ) ;
#159075=DIRECTION ( 'NONE',  ( -0.7071067811865463515, -0.7071067811865487940, -4.937700262164540154E-15 ) ) ;
#159094=ORIENTED_EDGE ( 'NONE', *, *, #161914, .F. ) ;
#159119=CARTESIAN_POINT ( 'NONE',  ( 17.74533788810829904, 65.18150020854140791, -146.8367301594720118 ) ) ;
#159295=DIRECTION ( 'NONE',  ( -0.000000000000000000, -6.982962677686266711E-15, 1.000000000000000000 ) ) ;
#159383=DIRECTION ( 'NONE',  ( 0.000000000000000000, -1.000000000000000000, -6.982962677686266711E-15 ) ) ;
#159450=EDGE_CURVE ( 'NONE', #105637, #77397, #141147, .T. ) ;
#159562=CARTESIAN_POINT ( 'NONE',  ( -16.80117486205003630, 66.05034273169992787, -149.1742526115989449 ) ) ;
#159622=AXIS2_PLACEMENT_3D ( 'NONE', #118362, #238280, #197873 ) ;
#159772=ORIENTED_EDGE ( 'NONE', *, *, #83834, .F. ) ;
#160195=DIRECTION ( 'NONE',  ( 1.000000000000000000, 0.000000000000000000, 0.000000000000000000 ) ) ;
#160357=CARTESIAN_POINT ( 'NONE',  ( -16.87331047859649757, 66.05000000001224691, -149.1731074845244223 ) ) ;
#160378=LINE ( 'NONE', #236030, #187253 ) ;
#160686=STYLED_ITEM ( 'NONE', ( #211907 ), #26318 ) ;
#160690=CARTESIAN_POINT ( 'NONE',  ( -18.40000000000000213, 67.17743825834591576, -160.7731074845244166 ) ) ;
#161169=VERTEX_POINT ( 'NONE', #144216 ) ;
#161193=ORIENTED_EDGE ( 'NONE', *, *, #208905, .T. ) ;
#161248=ADVANCED_FACE ( 'NONE', ( #256751 ), #78152, .F. ) ;
#161258=DIRECTION ( 'NONE',  ( 1.186688945009010077E-16, 1.000000000000000000, 6.982962677686266711E-15 ) ) ;
#161359=CARTESIAN_POINT ( 'NONE',  ( -16.87998658237755834, 66.05000000001230376, -157.1594679167859283 ) ) ;
#161435=CARTESIAN_POINT ( 'NONE',  ( -14.11697426661282506, 66.54258905524487488, -155.0230235107343333 ) ) ;
#161559=ADVANCED_FACE ( 'NONE', ( #164782 ), #141357, .F. ) ;
#161914=EDGE_CURVE ( 'NONE', #80617, #235459, #17926, .T. ) ;
#162094=PLANE ( 'NONE',  #163917 ) ;
#162312=ORIENTED_EDGE ( 'NONE', *, *, #76645, .T. ) ;
#162430=CARTESIAN_POINT ( 'NONE',  ( 16.87683809663750267, 66.05000000001230376, -157.3731074845244393 ) ) ;
#162438=ADVANCED_FACE ( 'NONE', ( #185373 ), #246620, .F. ) ;
#162634=UNCERTAINTY_MEASURE_WITH_UNIT (LENGTH_MEASURE( 1.000000000000000082E-05 ), #72395, 'distance_accuracy_value', 'NONE');
#162906=SURFACE_SIDE_STYLE ('',( #83306 ) ) ;
#162935=CARTESIAN_POINT ( 'NONE',  ( -21.64999999999999858, 66.65000000001225544, -149.1731074845244223 ) ) ;
#162945=CARTESIAN_POINT ( 'NONE',  ( -18.34374000495059676, 64.52683809664972614, -145.7731074845244450 ) ) ;
#163101=VECTOR ( 'NONE', #38603, 1000.000000000000000 ) ;
#163158=ORIENTED_EDGE ( 'NONE', *, *, #30381, .T. ) ;
#163532=CARTESIAN_POINT ( 'NONE',  ( -15.66061380678751291, 66.63927620602623847, -152.7091802899176116 ) ) ;
#163732=ORIENTED_EDGE ( 'NONE', *, *, #89019, .T. ) ;
#163917=AXIS2_PLACEMENT_3D ( 'NONE', #257266, #40875, #82504 ) ;
#164264=ORIENTED_EDGE ( 'NONE', *, *, #112094, .T. ) ;
#164726=CARTESIAN_POINT ( 'NONE',  ( -16.84421487269769102, 66.05000000001230376, -157.3536053620794632 ) ) ;
#164733=CARTESIAN_POINT ( 'NONE',  ( -16.93970660449832621, 65.98715860837673119, -157.4708257487299363 ) ) ;
#164761=( BOUNDED_CURVE ( )  B_SPLINE_CURVE ( 3, ( #240829, #101255, #102555, #2190 ),
 .UNSPECIFIED., .F., .F. ) 
 B_SPLINE_CURVE_WITH_KNOTS ( ( 4, 4 ),
 ( 0.3000847527772375622, 0.5517402753107888413 ),
 .UNSPECIFIED. ) 
 CURVE ( )  GEOMETRIC_REPRESENTATION_ITEM ( )  RATIONAL_B_SPLINE_CURVE ( ( 1.000000000000000000, 0.9947294176030464508, 0.9947294176030464508, 1.000000000000000000 ) ) 
 REPRESENTATION_ITEM ( '' )  );
#164782=FACE_OUTER_BOUND ( 'NONE', #233928, .T. ) ;
#164794=VECTOR ( 'NONE', #75695, 1000.000000000000000 ) ;
#164969=VERTEX_POINT ( 'NONE', #150079 ) ;
#165195=CARTESIAN_POINT ( 'NONE',  ( -16.83233564386414116, 66.06977820342760310, -157.2476281480000182 ) ) ;
#165238=CARTESIAN_POINT ( 'NONE',  ( -21.65000000000000213, 66.05000000001224691, -149.2731074845244450 ) ) ;
#165261=CARTESIAN_POINT ( 'NONE',  ( -15.75000000000000355, 66.65000000001228386, -153.2731074845243882 ) ) ;
#165310=ORIENTED_EDGE ( 'NONE', *, *, #25477, .T. ) ;
#165602=ORIENTED_EDGE ( 'NONE', *, *, #77361, .T. ) ;
#165841=EDGE_LOOP ( 'NONE', ( #18049, #247372, #121944, #183406 ) ) ;
#166127=ORIENTED_EDGE ( 'NONE', *, *, #257460, .T. ) ;
#166167=CARTESIAN_POINT ( 'NONE',  ( -15.75000000000000355, 66.15000000001228386, -153.2731074845244166 ) ) ;
#166217=DIRECTION ( 'NONE',  ( 0.000000000000000000, -6.982962677686266711E-15, 1.000000000000000000 ) ) ;
#166225=EDGE_CURVE ( 'NONE', #58960, #6078, #126835, .T. ) ;
#166284=CARTESIAN_POINT ( 'NONE',  ( -18.40000000000000213, 64.51332499825454647, -145.7731074845244450 ) ) ;
#166364=VERTEX_POINT ( 'NONE', #52416 ) ;
#166442=EDGE_CURVE ( 'NONE', #18925, #2008, #146, .T. ) ;
#166605=ORIENTED_EDGE ( 'NONE', *, *, #34144, .T. ) ;
#166627=VECTOR ( 'NONE', #196828, 1000.000000000000000 ) ;
#166716=( BOUNDED_CURVE ( )  B_SPLINE_CURVE ( 3, ( #203088, #24485, #243501, #223920 ),
 .UNSPECIFIED., .F., .F. ) 
 B_SPLINE_CURVE_WITH_KNOTS ( ( 4, 4 ),
 ( 0.3000847527772370071, 0.5497968875596834781 ),
 .UNSPECIFIED. ) 
 CURVE ( )  GEOMETRIC_REPRESENTATION_ITEM ( )  RATIONAL_B_SPLINE_CURVE ( ( 1.000000000000000000, 0.9948104011409417691, 0.9948104011409417691, 1.000000000000000000 ) ) 
 REPRESENTATION_ITEM ( '' )  );
#166930=CARTESIAN_POINT ( 'NONE',  ( 20.99999999999999645, 66.25000000001233502, -160.7731074845244166 ) ) ;
#166938=ORIENTED_EDGE ( 'NONE', *, *, #127580, .F. ) ;
#167186=CIRCLE ( 'NONE', #254418, 1.749999999999998002 ) ;
#167324=CARTESIAN_POINT ( 'NONE',  ( -16.93255653858138388, 66.00154854603513854, -157.4414641165347462 ) ) ;
#167527=ORIENTED_EDGE ( 'NONE', *, *, #73235, .T. ) ;
#167594=VERTEX_POINT ( 'NONE', #188451 ) ;
#167688=CARTESIAN_POINT ( 'NONE',  ( -17.22767730084089166, 65.65075578754372998, -158.6655361750987936 ) ) ;
#167756=CARTESIAN_POINT ( 'NONE',  ( -16.92507428761700439, 66.05000000001230376, -157.3097100249028699 ) ) ;
#167791=CARTESIAN_POINT ( 'NONE',  ( -16.82542659449973144, 66.06550010858485678, -157.2784718844984013 ) ) ;
#167802=DIRECTION ( 'NONE',  ( -1.000000000000000000, 0.000000000000000000, -0.000000000000000000 ) ) ;
#168350=VECTOR ( 'NONE', #11935, 1000.000000000000000 ) ;
#168435=DIRECTION ( 'NONE',  ( -1.000000000000000000, 0.000000000000000000, -0.000000000000000000 ) ) ;
#168453=CARTESIAN_POINT ( 'NONE',  ( 14.45963434102923806, 66.54845833862673032, -151.5692319856938468 ) ) ;
#168622=EDGE_LOOP ( 'NONE', ( #1895, #140294, #235360, #251429 ) ) ;
#168652=ORIENTED_EDGE ( 'NONE', *, *, #59452, .T. ) ;
#168773=ADVANCED_FACE ( 'NONE', ( #91962 ), #15017, .F. ) ;
#168987=CARTESIAN_POINT ( 'NONE',  ( -18.37013991200266005, 64.50025238380034409, -160.8161304950415627 ) ) ;
#169016=( LENGTH_UNIT ( ) NAMED_UNIT ( * ) SI_UNIT ( .MILLI., .METRE. ) );
#169089=CARTESIAN_POINT ( 'NONE',  ( -16.78055652883087134, 66.05322308388694807, -157.3623156469320179 ) ) ;
#169190=ORIENTED_EDGE ( 'NONE', *, *, #242400, .F. ) ;
#169209=AXIS2_PLACEMENT_3D ( 'NONE', #138353, #135795, #253182 ) ;
#169315=CARTESIAN_POINT ( 'NONE',  ( -16.91049119928363353, 66.05000000001231797, -157.4048278777152632 ) ) ;
#169533=ORIENTED_EDGE ( 'NONE', *, *, #45027, .F. ) ;
#169713=CARTESIAN_POINT ( 'NONE',  ( -16.87998658237729188, 66.05000000001223270, -149.3867470522638143 ) ) ;
#169740=LINE ( 'NONE', #148870, #241942 ) ;
#169874=DIRECTION ( 'NONE',  ( 1.000000000000000000, 0.000000000000000000, 0.000000000000000000 ) ) ;
#169925=AXIS2_PLACEMENT_3D ( 'NONE', #67274, #161258, #226322 ) ;
#170283=VECTOR ( 'NONE', #140782, 1000.000000000000000 ) ;
#170451=CARTESIAN_POINT ( 'NONE',  ( -12.84409460144757098, 66.58931770574434950, -154.5919640425762225 ) ) ;
#170607=VECTOR ( 'NONE', #191171, 1000.000000000000000 ) ;
#170615=CARTESIAN_POINT ( 'NONE',  ( 14.45204356427542614, 66.54933111084474717, -154.9675609943171253 ) ) ;
#170764=ORIENTED_EDGE ( 'NONE', *, *, #71559, .T. ) ;
#171006=CARTESIAN_POINT ( 'NONE',  ( -16.84793658983438291, 66.05000000001224691, -149.2567541623344312 ) ) ;
#171047=CARTESIAN_POINT ( 'NONE',  ( 23.04999999999999716, 67.17743825834580207, -145.7731074845244450 ) ) ;
#171210=CARTESIAN_POINT ( 'NONE',  ( -18.40000000000000213, 64.51332499825466016, -160.7731074845244450 ) ) ;
#171436=PLANE ( 'NONE',  #64751 ) ;
#171543=CARTESIAN_POINT ( 'NONE',  ( -18.41431012584568450, 64.51252797080414325, -160.7963434976261112 ) ) ;
#171671=DIRECTION ( 'NONE',  ( 0.7071067811865214825, -0.7071067811865735520, 0.000000000000000000 ) ) ;
#171855=ORIENTED_EDGE ( 'NONE', *, *, #11081, .T. ) ;
#172157=ORIENTED_EDGE ( 'NONE', *, *, #114741, .F. ) ;
#172220=VERTEX_POINT ( 'NONE', #184966 ) ;
#172286=CARTESIAN_POINT ( 'NONE',  ( -16.80621392010912629, 66.05779742250453523, -149.2126994499415957 ) ) ;
#172345=ORIENTED_EDGE ( 'NONE', *, *, #60269, .T. ) ;
#172602=ORIENTED_EDGE ( 'NONE', *, *, #245579, .F. ) ;
#172753=ORIENTED_EDGE ( 'NONE', *, *, #57374, .T. ) ;
#172805=( NAMED_UNIT ( * ) PLANE_ANGLE_UNIT ( ) SI_UNIT ( $, .RADIAN. ) );
#172856=EDGE_CURVE ( 'NONE', #254732, #98712, #75592, .T. ) ;
#173077=ORIENTED_EDGE ( 'NONE', *, *, #134582, .T. ) ;
#173094=ADVANCED_FACE ( 'NONE', ( #68854 ), #7580, .F. ) ;
#173177=CARTESIAN_POINT ( 'NONE',  ( 15.15590539855245922, 66.58931770574432107, -154.5919640425761941 ) ) ;
#173224=CARTESIAN_POINT ( 'NONE',  ( 20.04999999999999716, 67.25000000001222134, -149.1731074845244223 ) ) ;
#173280=AXIS2_PLACEMENT_3D ( 'NONE', #21949, #102726, #160195 ) ;
#173353=ORIENTED_EDGE ( 'NONE', *, *, #211524, .F. ) ;
#173534=CARTESIAN_POINT ( 'NONE',  ( -18.40000000000000213, 64.51332499825454647, -145.7731074845244450 ) ) ;
#173576=CARTESIAN_POINT ( 'NONE',  ( -16.83233564386387471, 66.06977820342763152, -149.2985868210483318 ) ) ;
#174056=CARTESIAN_POINT ( 'NONE',  ( -16.87683809663752399, 66.15000000001229807, -156.6207434663281219 ) ) ;
#174633=AXIS2_PLACEMENT_3D ( 'NONE', #103495, #102196, #24004 ) ;
#174736=ORIENTED_EDGE ( 'NONE', *, *, #180932, .F. ) ;
#174831=ORIENTED_EDGE ( 'NONE', *, *, #154816, .T. ) ;
#174988=EDGE_LOOP ( 'NONE', ( #184729, #128202, #21704, #227164 ) ) ;
#175314=CARTESIAN_POINT ( 'NONE',  ( -16.77683809663752257, 66.05416425680809311, -149.1870565036286109 ) ) ;
#175391=LINE ( 'NONE', #75006, #236636 ) ;
#175807=CARTESIAN_POINT ( 'NONE',  ( -16.94445028196807002, 66.00793639031451221, -149.1304376629428816 ) ) ;
#175846=CARTESIAN_POINT ( 'NONE',  ( -20.65000000000000568, 68.75000000001233502, -160.7731074845244166 ) ) ;
#175876=B_SPLINE_CURVE_WITH_KNOTS ( 'NONE', 3,
 ( #175807, #255265, #100068, #214909, #178379, #958, #197905, #77953, #76674, #21853, #257833, #216180, #199207 ),
 .UNSPECIFIED., .F., .F.,
 ( 4, 3, 3, 3, 4 ),
 ( -3.224855718275878119E-06, -4.235164736271501695E-22, 6.199515528669195097E-06, 4.034952380127538728E-05, 7.452715123699865944E-05 ),
 .UNSPECIFIED. ) ;
#176098=VECTOR ( 'NONE', #199589, 1000.000000000000000 ) ;
#176163=CARTESIAN_POINT ( 'NONE',  ( 12.84233041328156055, 66.58946139148339682, -154.5904194873835706 ) ) ;
#176223=ORIENTED_EDGE ( 'NONE', *, *, #25046, .F. ) ;
#176248=LINE ( 'NONE', #198349, #73944 ) ;
#176292=EDGE_CURVE ( 'NONE', #238447, #42338, #54246, .T. ) ;
#176593=CARTESIAN_POINT ( 'NONE',  ( -16.94878442675512886, 66.00827089702130479, -157.4113270601623071 ) ) ;
#176606=EDGE_CURVE ( 'NONE', #215723, #172220, #195857, .T. ) ;
#177011=DIRECTION ( 'NONE',  ( 0.000000000000000000, 6.982962677686266711E-15, -1.000000000000000000 ) ) ;
#177321=APPLICATION_CONTEXT ( 'automotive_design' ) ;
#177366=PLANE ( 'NONE',  #43710 ) ;
#177478=EDGE_CURVE ( 'NONE', #120061, #24865, #187230, .T. ) ;
#177575=CARTESIAN_POINT ( 'NONE',  ( -16.85312964099708566, 66.08639531794450761, -149.4202917780939686 ) ) ;
#177847=CARTESIAN_POINT ( 'NONE',  ( 21.13736287352038445, 67.95335762362829257, -157.3731074845244109 ) ) ;
#177972=CARTESIAN_POINT ( 'NONE',  ( -12.26136940704872202, 66.64859682587062650, -153.0435770476858579 ) ) ;
#177987=EDGE_CURVE ( 'NONE', #24865, #133198, #158319, .T. ) ;
#178180=CIRCLE ( 'NONE', #119937, 14.30833333333333890 ) ;
#178347=PLANE ( 'NONE',  #159622 ) ;
#178379=CARTESIAN_POINT ( 'NONE',  ( -16.94165728009536664, 66.01213024408845342, -149.1320524760142234 ) ) ;
#178518=CARTESIAN_POINT ( 'NONE',  ( -16.86578989773640913, 66.01519019875343020, -149.0584425979022001 ) ) ;
#178877=EDGE_LOOP ( 'NONE', ( #63019, #11769, #142206, #46878 ) ) ;
#178880=CARTESIAN_POINT ( 'NONE',  ( 23.04999999999999716, 67.17743825834591576, -160.7731074845244166 ) ) ;
#179034=LINE ( 'NONE', #138551, #141992 ) ;
#179134=ORIENTED_EDGE ( 'NONE', *, *, #222171, .T. ) ;
#179149=CARTESIAN_POINT ( 'NONE',  ( -16.78805706634180694, 66.05174750694105512, -149.1789542764925898 ) ) ;
#179170=CARTESIAN_POINT ( 'NONE',  ( -16.86445178670581058, 66.03778837089642195, -157.4138849226412731 ) ) ;
#179414=EDGE_LOOP ( 'NONE', ( #24206, #172345, #180905, #123663 ) ) ;
#179810=CARTESIAN_POINT ( 'NONE',  ( -16.81744102076749314, 66.05000000001230376, -157.3731074845244393 ) ) ;
#180061=ORIENTED_EDGE ( 'NONE', *, *, #32043, .T. ) ;
#180074=ADVANCED_FACE ( 'NONE', ( #99569 ), #10537, .T. ) ;
#180270=CARTESIAN_POINT ( 'NONE',  ( -16.79139129368505934, 66.05505583755062560, -157.3528628516985748 ) ) ;
#180471=B_SPLINE_CURVE_WITH_KNOTS ( 'NONE', 3,
 ( #32777, #131832, #229657, #133125, #93980, #212669, #207538, #28936, #253057, #11915, #150138, #168453, #14485, #52277, #250489, #108427, #34058, #247923, #191842, #69312, #50983, #208811, #73182, #74470, #9318, #187969, #31486, #88831, #151418, #130544 ),
 .UNSPECIFIED., .F., .F.,
 ( 4, 2, 2, 2, 2, 2, 2, 2, 2, 2, 2, 2, 2, 2, 4 ),
 ( 0.000000000000000000, 0.0003422764154113498236, 0.0006845528308226996473, 0.001026829246234049579, 0.001369105661645399295, 0.002053658492468046683, 0.002738211323290694072, 0.003080487738702019935, 0.003422764154113346231, 0.003765040569524672528, 0.004107316984935998824, 0.004449593400347324687, 0.004791869815758650550, 0.005134146231169977280, 0.005476422646581303143 ),
 .UNSPECIFIED. ) ;
#180485=CARTESIAN_POINT ( 'NONE',  ( -16.92989507731676824, 66.05000000001224691, -149.4056085539143055 ) ) ;
#180528=EDGE_CURVE ( 'NONE', #172220, #47223, #47064, .T. ) ;
#180651=ORIENTED_EDGE ( 'NONE', *, *, #215098, .F. ) ;
#180740=DIRECTION ( 'NONE',  ( 1.186688945009010077E-16, 1.000000000000000000, 6.982962677686266711E-15 ) ) ;
#180841=VECTOR ( 'NONE', #131824, 1000.000000000000000 ) ;
#180905=ORIENTED_EDGE ( 'NONE', *, *, #3437, .T. ) ;
#180913=FACE_OUTER_BOUND ( 'NONE', #25877, .T. ) ;
#180932=EDGE_CURVE ( 'NONE', #132836, #215608, #65001, .T. ) ;
#181174=FILL_AREA_STYLE_COLOUR ( '', #204536 ) ;
#181569=CARTESIAN_POINT ( 'NONE',  ( -16.81453046979148880, 66.06089771857138260, -157.3113809609213831 ) ) ;
#181645=ORIENTED_EDGE ( 'NONE', *, *, #185926, .T. ) ;
#181702=EDGE_LOOP ( 'NONE', ( #3007, #130593, #13498 ) ) ;
#181810=CARTESIAN_POINT ( 'NONE',  ( -14.22969084473440304, 66.54399267394295236, -151.5344739903776485 ) ) ;
#181900=ORIENTED_EDGE ( 'NONE', *, *, #176606, .T. ) ;
#182125=AXIS2_PLACEMENT_3D ( 'NONE', #189125, #52165, #228262 ) ;
#182200=CARTESIAN_POINT ( 'NONE',  ( -16.97683809663752186, 66.05000000001230376, -156.6207434663279230 ) ) ;
#182282=FACE_OUTER_BOUND ( 'NONE', #178877, .T. ) ;
#182353=CARTESIAN_POINT ( 'NONE',  ( -16.87786941232800686, 66.04184528586726799, -149.1459216847304390 ) ) ;
#182436=CARTESIAN_POINT ( 'NONE',  ( 20.73486653747088937, 68.25000000001227818, -157.3731074845244109 ) ) ;
#182698=EDGE_LOOP ( 'NONE', ( #111989, #171855, #189181 ) ) ;
#183023=CARTESIAN_POINT ( 'NONE',  ( -16.93339986808596720, 65.99489607144637660, -157.4571138127115830 ) ) ;
#183037=ORIENTED_EDGE ( 'NONE', *, *, #107575, .T. ) ;
#183066=EDGE_LOOP ( 'NONE', ( #186206, #203153, #1532, #105648 ) ) ;
#183108=CARTESIAN_POINT ( 'NONE',  ( -15.06720934482786411, 66.58230930894919197, -151.8815067877598608 ) ) ;
#183213=ORIENTED_EDGE ( 'NONE', *, *, #177987, .T. ) ;
#183389=CARTESIAN_POINT ( 'NONE',  ( 15.48841904831874849, 67.43841904833101353, -149.1731074845244223 ) ) ;
#183406=ORIENTED_EDGE ( 'NONE', *, *, #180932, .T. ) ;
#183551=CARTESIAN_POINT ( 'NONE',  ( -13.88555196119804869, 66.54256847116334939, -155.0231905466248179 ) ) ;
#183714=AXIS2_PLACEMENT_3D ( 'NONE', #21539, #38526, #18944 ) ;
#183910=CARTESIAN_POINT ( 'NONE',  ( 18.54999999999999716, 66.05000000001223270, -149.1731074845243654 ) ) ;
#184059=LINE ( 'NONE', #79802, #140836 ) ;
#184074=ORIENTED_EDGE ( 'NONE', *, *, #58026, .F. ) ;
#184230=ORIENTED_EDGE ( 'NONE', *, *, #161914, .T. ) ;
#184435=VERTEX_POINT ( 'NONE', #177847 ) ;
#184500=LINE ( 'NONE', #85374, #65212 ) ;
#184729=ORIENTED_EDGE ( 'NONE', *, *, #166225, .F. ) ;
#184853=DIRECTION ( 'NONE',  ( -1.186688945009010077E-16, -1.000000000000000000, -6.982962677686266711E-15 ) ) ;
#184966=CARTESIAN_POINT ( 'NONE',  ( -17.11825945287482753, 65.95000000001232365, -157.3731074845244393 ) ) ;
#184986=CARTESIAN_POINT ( 'NONE',  ( -17.01764560440407692, 66.05000000001231797, -157.2731074853133180 ) ) ;
#185061=LINE ( 'NONE', #6422, #86612 ) ;
#185373=FACE_OUTER_BOUND ( 'NONE', #174988, .T. ) ;
#185671=VECTOR ( 'NONE', #93823, 1000.000000000000000 ) ;
#185926=EDGE_CURVE ( 'NONE', #246673, #18925, #46366, .T. ) ;
#185936=ORIENTED_EDGE ( 'NONE', *, *, #4097, .F. ) ;
#186062=EDGE_CURVE ( 'NONE', #128197, #114211, #138409, .T. ) ;
#186206=ORIENTED_EDGE ( 'NONE', *, *, #159450, .F. ) ;
#186229=ORIENTED_EDGE ( 'NONE', *, *, #245579, .T. ) ;
#186345=VECTOR ( 'NONE', #89372, 1000.000000000000000 ) ;
#186390=CARTESIAN_POINT ( 'NONE',  ( 18.39999999999999503, 70.35000000001230092, -157.3731074845244109 ) ) ;
#186604=CARTESIAN_POINT ( 'NONE',  ( 21.13736287352038445, 67.95335762362832099, -160.7731074845244166 ) ) ;
#186710=CARTESIAN_POINT ( 'NONE',  ( -16.94107738177414291, 65.98576071487562444, -149.0731074845244279 ) ) ;
#186824=AXIS2_PLACEMENT_3D ( 'NONE', #126926, #82620, #124365 ) ;
#186872=DIRECTION ( 'NONE',  ( 1.000000000000000000, 0.000000000000000000, 0.000000000000000000 ) ) ;
#187001=ORIENTED_EDGE ( 'NONE', *, *, #210862, .T. ) ;
#187221=( BOUNDED_CURVE ( )  B_SPLINE_CURVE ( 3, ( #135970, #134684, #211697, #214248 ),
 .UNSPECIFIED., .F., .F. ) 
 B_SPLINE_CURVE_WITH_KNOTS ( ( 4, 4 ),
 ( 3.752122642744585068, 4.712388980384675463 ),
 .UNSPECIFIED. ) 
 CURVE ( )  GEOMETRIC_REPRESENTATION_ITEM ( )  RATIONAL_B_SPLINE_CURVE ( ( 1.000000000000000000, 0.9246222802177217481, 0.9246222802177217481, 1.000000000000000000 ) ) 
 REPRESENTATION_ITEM ( '' )  );
#187230=LINE ( 'NONE', #64686, #186345 ) ;
#187253=VECTOR ( 'NONE', #19565, 1000.000000000000000 ) ;
#187451=CARTESIAN_POINT ( 'NONE',  ( 13.99999999999999822, 66.15000000001228386, -153.2731074845244450 ) ) ;
#187580=DIRECTION ( 'NONE',  ( -1.000000000000000000, 0.000000000000000000, 0.000000000000000000 ) ) ;
#187887=AXIS2_PLACEMENT_3D ( 'NONE', #131532, #12899, #28639 ) ;
#187969=CARTESIAN_POINT ( 'NONE',  ( 12.33938619321247998, 66.63927620602625268, -152.7091802899177537 ) ) ;
#188009=ORIENTED_EDGE ( 'NONE', *, *, #242721, .F. ) ;
#188014=CARTESIAN_POINT ( 'NONE',  ( 20.99999999999999645, 66.25000000001230660, -157.3731074845244393 ) ) ;
#188073=VECTOR ( 'NONE', #130169, 1000.000000000000000 ) ;
#188451=CARTESIAN_POINT ( 'NONE',  ( -18.40000000000000213, 64.25000000001222134, -145.7731074845244450 ) ) ;
#188600=CARTESIAN_POINT ( 'NONE',  ( -16.87401514999223195, 66.05000000001230376, -157.3031254770564829 ) ) ;
#188609=CARTESIAN_POINT ( 'NONE',  ( -17.11825945287481332, 65.95000000001225260, -149.2731074845244450 ) ) ;
#188627=EDGE_CURVE ( 'NONE', #151479, #84754, #187221, .T. ) ;
#188662=CARTESIAN_POINT ( 'NONE',  ( 18.54999999999999716, 52.34166666667894674, -153.2731074845245303 ) ) ;
#189049=CARTESIAN_POINT ( 'NONE',  ( -16.89318236219974523, 66.04846474213709939, -149.1679778524185735 ) ) ;
#189125=CARTESIAN_POINT ( 'NONE',  ( 20.73486653747088937, 68.25000000001229239, -160.7731074845244166 ) ) ;
#189181=ORIENTED_EDGE ( 'NONE', *, *, #232710, .F. ) ;
#189278=LINE ( 'NONE', #88856, #168350 ) ;
#189779=CARTESIAN_POINT ( 'NONE',  ( -16.94107738177414291, 65.98576071487562444, -149.0731074845244279 ) ) ;
#189846=EDGE_LOOP ( 'NONE', ( #43041, #179134, #173353, #151392 ) ) ;
#189963=VERTEX_POINT ( 'NONE', #204966 ) ;
#189976=VERTEX_POINT ( 'NONE', #6785 ) ;
#190046=ADVANCED_FACE ( 'NONE', ( #249259 ), #129306, .F. ) ;
#190130=CARTESIAN_POINT ( 'NONE',  ( -16.95709691156827148, 66.05000000001231797, -157.3630499220105037 ) ) ;
#190171=LINE ( 'NONE', #192737, #188073 ) ;
#190350=CARTESIAN_POINT ( 'NONE',  ( -16.90202395485809816, 66.03405545546122823, -149.1200937632631565 ) ) ;
#190387=ORIENTED_EDGE ( 'NONE', *, *, #12080, .T. ) ;
#190438=CARTESIAN_POINT ( 'NONE',  ( -17.01473183483379970, 66.05000000001224691, -149.2731074845244450 ) ) ;
#190444=DIRECTION ( 'NONE',  ( -0.000000000000000000, -6.982962677686266711E-15, 1.000000000000000000 ) ) ;
#190476=ADVANCED_FACE ( 'NONE', ( #55844 ), #54587, .F. ) ;
#190541=CARTESIAN_POINT ( 'NONE',  ( -16.96982749440682525, 66.05000000001224691, -149.6478858933352001 ) ) ;
#190821=EDGE_LOOP ( 'NONE', ( #172602, #205803, #43198, #39491, #233602 ) ) ;
#190951=ADVANCED_FACE ( 'NONE', ( #11307 ), #192510, .F. ) ;
#191026=VERTEX_POINT ( 'NONE', #70870 ) ;
#191151=ORIENTED_EDGE ( 'NONE', *, *, #112439, .F. ) ;
#191171=DIRECTION ( 'NONE',  ( -1.020425574104004196E-15, -6.982962677686266711E-15, 1.000000000000000000 ) ) ;
#191440=CARTESIAN_POINT ( 'NONE',  ( 14.56326696814971733, 66.55335100938343373, -154.9339441886012310 ) ) ;
#191457=( BOUNDED_CURVE ( )  B_SPLINE_CURVE ( 3, ( #252314, #13719, #32028, #253598 ),
 .UNSPECIFIED., .F., .T. ) 
 B_SPLINE_CURVE_WITH_KNOTS ( ( 4, 4 ),
 ( 2.589852378279005496, 2.850972632318389710 ),
 .UNSPECIFIED. ) 
 CURVE ( )  GEOMETRIC_REPRESENTATION_ITEM ( )  RATIONAL_B_SPLINE_CURVE ( ( 1.000000000000000000, 0.9943260843901261525, 0.9943260843901261525, 1.000000000000000000 ) ) 
 REPRESENTATION_ITEM ( '' )  );
#191468=ORIENTED_EDGE ( 'NONE', *, *, #177478, .T. ) ;
#191625=ORIENTED_EDGE ( 'NONE', *, *, #132721, .T. ) ;
#191695=VECTOR ( 'NONE', #84217, 999.9999999999998863 ) ;
#191772=SHAPE_DEFINITION_REPRESENTATION ( #91051, #10216 ) ;
#191842=CARTESIAN_POINT ( 'NONE',  ( 13.12229106158774883, 66.56936289831551790, -151.7548468664635095 ) ) ;
#192056=EDGE_LOOP ( 'NONE', ( #187001, #231703, #228063, #215940 ) ) ;
#192155=ORIENTED_EDGE ( 'NONE', *, *, #59452, .F. ) ;
#192389=DIRECTION ( 'NONE',  ( -0.5932847527679299127, -0.8049926720990051576, -6.257843056355997642E-15 ) ) ;
#192466=CARTESIAN_POINT ( 'NONE',  ( -16.79184697841823848, 66.05123833835389746, -157.3689652139219106 ) ) ;
#192474=EDGE_CURVE ( 'NONE', #244466, #240031, #79414, .T. ) ;
#192501=APPLICATION_CONTEXT ( 'automotive_design' ) ;
#192510=PLANE ( 'NONE',  #3531 ) ;
#192695=CARTESIAN_POINT ( 'NONE',  ( 14.77516762759922386, 66.56332574816944714, -154.8462455535252502 ) ) ;
#192737=CARTESIAN_POINT ( 'NONE',  ( 20.73486653747088226, 68.75000000001227818, -157.3731074845244109 ) ) ;
#193096=CARTESIAN_POINT ( 'NONE',  ( -16.89935556175703368, 66.05000000001224691, -149.6627838474101964 ) ) ;
#193892=CARTESIAN_POINT ( 'NONE',  ( -17.71734398241074970, 65.15764277154774220, -159.7482457375300555 ) ) ;
#193933=ORIENTED_EDGE ( 'NONE', *, *, #166225, .T. ) ;
#193996=CARTESIAN_POINT ( 'NONE',  ( -16.95709691156811871, 66.05000000001224691, -149.1831650470383295 ) ) ;
#194214=CIRCLE ( 'NONE', #98460, 14.30833333333333890 ) ;
#194237=MANIFOLD_SOLID_BREP ( 'Stock-MAS-200-1', #3354 ) ;
#194365=CARTESIAN_POINT ( 'NONE',  ( -17.29838795457901313, 65.62845014207074712, -147.9183662019067640 ) ) ;
#194393=CARTESIAN_POINT ( 'NONE',  ( -16.87683809663752044, 66.05000000001224691, -149.9254715027207396 ) ) ;
#194528=FACE_OUTER_BOUND ( 'NONE', #85884, .T. ) ;
#194755=AXIS2_PLACEMENT_3D ( 'NONE', #103969, #124851, #123564 ) ;
#194776=EDGE_CURVE ( 'NONE', #14807, #6078, #234372, .T. ) ;
#194815=DIRECTION ( 'NONE',  ( 0.000000000000000000, -6.982962677686266711E-15, 1.000000000000000000 ) ) ;
#194912=( NAMED_UNIT ( * ) SI_UNIT ( $, .STERADIAN. ) SOLID_ANGLE_UNIT ( ) );
#194988=CARTESIAN_POINT ( 'NONE',  ( -18.35663730107557257, 64.52609257350111704, -160.7731074845244450 ) ) ;
#195013=CARTESIAN_POINT ( 'NONE',  ( -18.40000000000000213, 64.25000000001230660, -157.3731074845244393 ) ) ;
#195136=CARTESIAN_POINT ( 'NONE',  ( -23.25000000000000355, 64.25000000001233502, -160.7731074845244450 ) ) ;
#195280=CARTESIAN_POINT ( 'NONE',  ( 15.74999999999999289, 66.65000000001225544, -153.5045385271216958 ) ) ;
#195657=EDGE_CURVE ( 'NONE', #80528, #122105, #34320, .T. ) ;
#195731=CARTESIAN_POINT ( 'NONE',  ( 13.43443725621852103, 66.55344247693975035, -154.9331655301785133 ) ) ;
#195857=LINE ( 'NONE', #129749, #46525 ) ;
#196057=ORIENTED_EDGE ( 'NONE', *, *, #230996, .F. ) ;
#196136=CARTESIAN_POINT ( 'NONE',  ( -16.92778301347243897, 65.99905508317739589, -157.4516255924938832 ) ) ;
#196268=DIRECTION ( 'NONE',  ( -1.000000000000000000, 0.000000000000000000, -0.000000000000000000 ) ) ;
#196307=VERTEX_POINT ( 'NONE', #128598 ) ;
#196681=CARTESIAN_POINT ( 'NONE',  ( -16.87845715379269507, 66.04214188611527447, -157.3993068334655447 ) ) ;
#196736=CARTESIAN_POINT ( 'NONE',  ( -16.81744102076748959, 66.05000000001224691, -149.1731074845244223 ) ) ;
#196828=DIRECTION ( 'NONE',  ( 0.000000000000000000, 1.000000000000000000, 6.982962677686266711E-15 ) ) ;
#196941=CARTESIAN_POINT ( 'NONE',  ( 16.27683809663749770, 66.65000000001234071, -160.7731074845244166 ) ) ;
#196964=CIRCLE ( 'NONE', #55461, 1.749999999999999778 ) ;
#196974=CARTESIAN_POINT ( 'NONE',  ( -18.35668295345803713, 64.52683809664974035, -145.7731074845244450 ) ) ;
#196999=AXIS2_PLACEMENT_3D ( 'NONE', #38436, #94546, #114111 ) ;
#197004=DIRECTION ( 'NONE',  ( -1.000000000000000000, 0.000000000000000000, -0.000000000000000000 ) ) ;
#197130=CARTESIAN_POINT ( 'NONE',  ( -18.39999999999999858, 64.52683809664983983, -160.7232782360584338 ) ) ;
#197214=FACE_BOUND ( 'NONE', #129031, .T. ) ;
#197448=SHAPE_REPRESENTATION_RELATIONSHIP ( 'NONE' , 'NONE' ,  #10216, #26318 ) ;
#197602=DIRECTION ( 'NONE',  ( 0.7071067811865463515, 0.7071067811865487940, 4.937700262164540154E-15 ) ) ;
#197873=DIRECTION ( 'NONE',  ( 0.000000000000000000, -6.982962677686266711E-15, 1.000000000000000000 ) ) ;
#197905=CARTESIAN_POINT ( 'NONE',  ( -16.93935632781549572, 66.01526950028714680, -149.1334467358141467 ) ) ;
#198220=DIRECTION ( 'NONE',  ( 0.000000000000000000, -1.000000000000000000, -6.982962677686266711E-15 ) ) ;
#198301=DIRECTION ( 'NONE',  ( -0.000000000000000000, -6.982962677686266711E-15, 1.000000000000000000 ) ) ;
#198349=CARTESIAN_POINT ( 'NONE',  ( -21.65000000000000213, 68.75000000001232081, -157.3731074845244109 ) ) ;
#198378=CARTESIAN_POINT ( 'NONE',  ( -16.85939681242905763, 66.09477481408694644, -149.4831855293329284 ) ) ;
#198634=DIRECTION ( 'NONE',  ( 0.7071067811865493491, -0.7071067811865456854, -4.937700262164518065E-15 ) ) ;
#198699=CARTESIAN_POINT ( 'NONE',  ( -16.89318236219977010, 66.04846474213715624, -157.3782371166302880 ) ) ;
#198931=ORIENTED_EDGE ( 'NONE', *, *, #230436, .F. ) ;
#199023=DIRECTION ( 'NONE',  ( -3.035766082959430717E-14, -6.982962677686266711E-15, 1.000000000000000000 ) ) ;
#199139=ADVANCED_FACE ( 'NONE', ( #127941 ), #208770, .F. ) ;
#199207=CARTESIAN_POINT ( 'NONE',  ( -16.89268316805465986, 66.04827818677006235, -149.1673550059788909 ) ) ;
#199311=DIRECTION ( 'NONE',  ( -0.000000000000000000, -6.982962677686266711E-15, 1.000000000000000000 ) ) ;
#199323=ADVANCED_FACE ( 'NONE', ( #92648 ), #177366, .F. ) ;
#199356=AXIS2_PLACEMENT_3D ( 'NONE', #13708, #232778, #11148 ) ;
#199589=DIRECTION ( 'NONE',  ( -0.5932847527679310229, -0.8049926720990042694, -4.984624513800578906E-15 ) ) ;
#199614=EDGE_LOOP ( 'NONE', ( #215353, #76800, #209014, #92125 ) ) ;
#199849=CARTESIAN_POINT ( 'NONE',  ( -16.85939591225058010, 66.09477352162440411, -157.0630392380553531 ) ) ;
#200089=DIRECTION ( 'NONE',  ( 0.000000000000000000, 0.000000000000000000, 1.000000000000000000 ) ) ;
#200297=CYLINDRICAL_SURFACE ( 'NONE', #88552, 1.749999999999998002 ) ;
#200390=CARTESIAN_POINT ( 'NONE',  ( 23.04999999999999716, 67.17743825834588733, -157.3731074845244109 ) ) ;
#200726=CARTESIAN_POINT ( 'NONE',  ( 18.39999999999999503, 67.17743825834580207, -145.7731074845244450 ) ) ;
#200957=ORIENTED_EDGE ( 'NONE', *, *, #3430, .F. ) ;
#200969=FACE_OUTER_BOUND ( 'NONE', #222012, .T. ) ;
#200985=CYLINDRICAL_SURFACE ( 'NONE', #182125, 0.5000000000000004441 ) ;
#201009=( BOUNDED_CURVE ( )  B_SPLINE_CURVE ( 3, ( #152605, #190438, #73077, #70504 ),
 .UNSPECIFIED., .F., .F. ) 
 B_SPLINE_CURVE_WITH_KNOTS ( ( 4, 4 ),
 ( 1.570796326794908992, 2.617993877991549034 ),
 .UNSPECIFIED. ) 
 CURVE ( )  GEOMETRIC_REPRESENTATION_ITEM ( )  RATIONAL_B_SPLINE_CURVE ( ( 1.000000000000000000, 0.9106836025229521070, 0.9106836025229521070, 1.000000000000000000 ) ) 
 REPRESENTATION_ITEM ( '' )  );
#201069=DIRECTION ( 'NONE',  ( 0.000000000000000000, -6.789366196018718420E-15, 1.000000000000000000 ) ) ;
#201310=( BOUNDED_CURVE ( )  B_SPLINE_CURVE ( 3, ( #204185, #67253, #86797, #226303 ),
 .UNSPECIFIED., .F., .T. ) 
 B_SPLINE_CURVE_WITH_KNOTS ( ( 4, 4 ),
 ( 1.570796326794892339, 3.141592653589784678 ),
 .UNSPECIFIED. ) 
 CURVE ( )  GEOMETRIC_REPRESENTATION_ITEM ( )  RATIONAL_B_SPLINE_CURVE ( ( 1.000000000000000000, 0.8047378541243659367, 0.8047378541243659367, 1.000000000000000000 ) ) 
 REPRESENTATION_ITEM ( '' )  );
#201378=VERTEX_POINT ( 'NONE', #14842 ) ;
#201549=AXIS2_PLACEMENT_3D ( 'NONE', #188609, #167802, #149516 ) ;
#201743=UNCERTAINTY_MEASURE_WITH_UNIT (LENGTH_MEASURE( 1.000000000000000082E-05 ), #93212, 'distance_accuracy_value', 'NONE');
#202072=CARTESIAN_POINT ( 'NONE',  ( 21.72449340488910252, 65.71604372252119219, -160.7731074845244166 ) ) ;
#202230=ORIENTED_EDGE ( 'NONE', *, *, #115796, .T. ) ;
#202571=CARTESIAN_POINT ( 'NONE',  ( -16.93658211146646408, 66.00589133767111605, -157.4274025544800963 ) ) ;
#202610=CARTESIAN_POINT ( 'NONE',  ( -16.94226253665225101, 66.05000000001226113, -149.4698420801402392 ) ) ;
#202649=CARTESIAN_POINT ( 'NONE',  ( -14.77538296656413586, 66.56333706821317264, -151.7000707522295215 ) ) ;
#202774=CARTESIAN_POINT ( 'NONE',  ( -15.75000000000000355, 66.15000000001228386, -153.2731074845244166 ) ) ;
#202864=ORIENTED_EDGE ( 'NONE', *, *, #6358, .T. ) ;
#203026=CARTESIAN_POINT ( 'NONE',  ( -16.87683809663750623, 66.05000000001230376, -156.6207434663279230 ) ) ;
#203088=CARTESIAN_POINT ( 'NONE',  ( -16.94107738177415712, 65.98576071487568129, -157.4731074845244336 ) ) ;
#203153=ORIENTED_EDGE ( 'NONE', *, *, #73235, .F. ) ;
#203174=CARTESIAN_POINT ( 'NONE',  ( 18.39999999999999503, 64.25000000001224976, -149.1731074845244507 ) ) ;
#203214=CARTESIAN_POINT ( 'NONE',  ( -16.90257928357874206, 66.04589317890692257, -157.3868220544107430 ) ) ;
#203447=AXIS2_PLACEMENT_3D ( 'NONE', #213884, #153965, #96482 ) ;
#203480=CARTESIAN_POINT ( 'NONE',  ( -23.25000000000000355, 64.25000000001222134, -145.7731074845244450 ) ) ;
#203802=CARTESIAN_POINT ( 'NONE',  ( -23.25000000000000355, 64.25000000001230660, -157.3731074845244393 ) ) ;
#203810=CARTESIAN_POINT ( 'NONE',  ( -16.77732147262506146, 66.05403306739360403, -149.1866162412485437 ) ) ;
#203826=CARTESIAN_POINT ( 'NONE',  ( 12.25000000000000000, 66.15000000001228386, -153.2731074845244450 ) ) ;
#203830=ADVANCED_FACE ( 'NONE', ( #223437 ), #46087, .F. ) ;
#203845=CARTESIAN_POINT ( 'NONE',  ( -16.94180778212363236, 66.00755694428015374, -157.4189239139911649 ) ) ;
#203884=CARTESIAN_POINT ( 'NONE',  ( -16.97683809663752186, 66.05000000001226113, -149.9254715027207681 ) ) ;
#204185=CARTESIAN_POINT ( 'NONE',  ( -18.40000000000000213, 64.66825945288714195, -157.3731074845244393 ) ) ;
#204302=CARTESIAN_POINT ( 'NONE',  ( -16.77180007708461673, 66.05000000001230376, -157.3874933655695827 ) ) ;
#204380=ORIENTED_EDGE ( 'NONE', *, *, #207763, .T. ) ;
#204506=DIRECTION ( 'NONE',  ( 0.000000000000000000, -1.000000000000000000, -6.982962677686266711E-15 ) ) ;
#204536=COLOUR_RGB ( '', 0.72549020, 0.75294118, 0.79215686) ;
#204771=ORIENTED_EDGE ( 'NONE', *, *, #127580, .T. ) ;
#204839=CARTESIAN_POINT ( 'NONE',  ( 20.27550659511089037, 66.78395627750344943, -157.3731074845244393 ) ) ;
#204966=CARTESIAN_POINT ( 'NONE',  ( -16.89268316805465986, 66.04827818677006235, -149.1673550059788909 ) ) ;
#205107=CARTESIAN_POINT ( 'NONE',  ( -16.81744102076749314, 66.05000000001230376, -157.3731074845244393 ) ) ;
#205585=CARTESIAN_POINT ( 'NONE',  ( -16.80621392010918314, 66.05779742250456366, -157.3335155191072374 ) ) ;
#205656=CARTESIAN_POINT ( 'NONE',  ( -15.75000000000000000, 66.65000000001228386, -153.5015881126992667 ) ) ;
#205803=ORIENTED_EDGE ( 'NONE', *, *, #115170, .F. ) ;
#205895=CIRCLE ( 'NONE', #93455, 0.1999999999999987899 ) ;
#205934=PLANE ( 'NONE',  #8806 ) ;
#206069=VECTOR ( 'NONE', #107144, 1000.000000000000000 ) ;
#206277=EDGE_LOOP ( 'NONE', ( #169533, #101188, #234928, #23513, #162312 ) ) ;
#206492=ORIENTED_EDGE ( 'NONE', *, *, #107575, .F. ) ;
#206886=UNCERTAINTY_MEASURE_WITH_UNIT (LENGTH_MEASURE( 1.000000000000000082E-05 ), #169016, 'distance_accuracy_value', 'NONE');
#207080=EDGE_CURVE ( 'NONE', #235459, #98712, #180471, .T. ) ;
#207104=DIRECTION ( 'NONE',  ( 0.7071067811865456854, 0.7071067811865493491, 4.937700262164544098E-15 ) ) ;
#207193=DIRECTION ( 'NONE',  ( 1.000000000000000000, 0.000000000000000000, 0.000000000000000000 ) ) ;
#207236=DIRECTION ( 'NONE',  ( -1.020425574104004196E-15, 6.982962677686266711E-15, -1.000000000000000000 ) ) ;
#207538=CARTESIAN_POINT ( 'NONE',  ( 15.51872946208853499, 66.62341902196831711, -152.3961612375124730 ) ) ;
#207574=DIRECTION ( 'NONE',  ( -1.646408749285562691E-14, -1.000000000000000000, -6.982962677686266711E-15 ) ) ;
#207617=CARTESIAN_POINT ( 'NONE',  ( -17.11825945287481332, 65.95000000001225260, -149.1731074845244223 ) ) ;
#207763=EDGE_CURVE ( 'NONE', #67597, #225539, #196964, .T. ) ;
#208093=CARTESIAN_POINT ( 'NONE',  ( -17.78241384945270909, 65.14442424721120517, -159.7740698120441891 ) ) ;
#208341=EDGE_CURVE ( 'NONE', #98712, #235459, #226609, .T. ) ;
#208566=EDGE_CURVE ( 'NONE', #221781, #166364, #205895, .T. ) ;
#208770=CYLINDRICAL_SURFACE ( 'NONE', #214395, 0.9000000000000014655 ) ;
#208811=CARTESIAN_POINT ( 'NONE',  ( 12.68104795156995479, 66.60346600605836898, -152.1171677053511360 ) ) ;
#208833=CIRCLE ( 'NONE', #154874, 0.9000000000000014655 ) ;
#208905=EDGE_CURVE ( 'NONE', #189963, #53606, #251063, .T. ) ;
#209014=ORIENTED_EDGE ( 'NONE', *, *, #30014, .T. ) ;
#209303=LINE ( 'NONE', #88048, #156890 ) ;
#209466=EDGE_CURVE ( 'NONE', #13430, #257702, #254492, .T. ) ;
#209737=DIRECTION ( 'NONE',  ( 1.186688945009009831E-16, 1.000000000000000000, 6.982962677686266711E-15 ) ) ;
#209883=DIRECTION ( 'NONE',  ( -0.000000000000000000, -6.982962677686266711E-15, 1.000000000000000000 ) ) ;
#210098=CARTESIAN_POINT ( 'NONE',  ( -16.85722902420161518, 66.05000000001224691, -149.2886549582941882 ) ) ;
#210133=DIRECTION ( 'NONE',  ( 0.000000000000000000, 6.982962677686266711E-15, -1.000000000000000000 ) ) ;
#210216=AXIS2_PLACEMENT_3D ( 'NONE', #28975, #148885, #108462 ) ;
#210251=LINE ( 'NONE', #131978, #77831 ) ;
#210252=CARTESIAN_POINT ( 'NONE',  ( -16.87435696428308063, 66.04999753708007404, -157.3731157193578554 ) ) ;
#210270=VERTEX_POINT ( 'NONE', #49288 ) ;
#210742=CARTESIAN_POINT ( 'NONE',  ( -16.81744102076749314, 66.05000000001230376, -157.3731074845244393 ) ) ;
#210862=EDGE_CURVE ( 'NONE', #120061, #53606, #218699, .T. ) ;
#211379=ORIENTED_EDGE ( 'NONE', *, *, #12080, .F. ) ;
#211524=EDGE_CURVE ( 'NONE', #164969, #48358, #242079, .T. ) ;
#211697=CARTESIAN_POINT ( 'NONE',  ( -17.04761207306817283, 65.97354912661445780, -149.1731074845244507 ) ) ;
#211817=DIRECTION ( 'NONE',  ( 0.000000000000000000, 1.000000000000000000, 6.982962677686266711E-15 ) ) ;
#211907=PRESENTATION_STYLE_ASSIGNMENT (( #35835 ) ) ;
#211937=EDGE_LOOP ( 'NONE', ( #147998, #186229, #225624, #154013, #126581, #255120 ) ) ;
#211950=CYLINDRICAL_SURFACE ( 'NONE', #91885, 1.749999999999999778 ) ;
#212315=DIRECTION ( 'NONE',  ( -1.073024830501117725E-15, 6.982962677686266711E-15, -1.000000000000000000 ) ) ;
#212571=ORIENTED_EDGE ( 'NONE', *, *, #142449, .T. ) ;
#212669=CARTESIAN_POINT ( 'NONE',  ( 15.57250062127603130, 66.62931007840965947, -152.4966423578634078 ) ) ;
#212783=ADVANCED_FACE ( 'NONE', ( #236724 ), #217153, .F. ) ;
#213189=CARTESIAN_POINT ( 'NONE',  ( -17.29838795460002032, 65.62845014204981453, -158.6278487671399375 ) ) ;
#213216=LINE ( 'NONE', #132418, #67788 ) ;
#213271=CARTESIAN_POINT ( 'NONE',  ( -16.87683809663752399, 66.15000000001231228, -157.3731074845244393 ) ) ;
#213296=CARTESIAN_POINT ( 'NONE',  ( -16.77683809663752257, 66.05416425680813575, -157.3591584654202222 ) ) ;
#213297=EDGE_CURVE ( 'NONE', #232094, #139384, #61783, .T. ) ;
#213382=LINE ( 'NONE', #34791, #15172 ) ;
#213383=ADVANCED_FACE ( 'NONE', ( #114906 ), #90802, .T. ) ;
#213620=ORIENTED_EDGE ( 'NONE', *, *, #11627, .T. ) ;
#213629=EDGE_CURVE ( 'NONE', #133198, #127404, #65196, .T. ) ;
#213832=LINE ( 'NONE', #117305, #166627 ) ;
#213884=CARTESIAN_POINT ( 'NONE',  ( -16.97683809663752186, 66.15000000001231228, -157.3731074845244393 ) ) ;
#213930=CARTESIAN_POINT ( 'NONE',  ( -16.88705144915421030, 66.05000000001224691, -149.4540860792365322 ) ) ;
#214248=CARTESIAN_POINT ( 'NONE',  ( -17.11825945287481332, 65.95000000001225260, -149.1731074845244223 ) ) ;
#214395=AXIS2_PLACEMENT_3D ( 'NONE', #150089, #10567, #126650 ) ;
#214490=DIRECTION ( 'NONE',  ( 1.000000000000000000, 0.000000000000000000, 0.000000000000000000 ) ) ;
#214768=DIRECTION ( 'NONE',  ( -0.7071067811865463515, 0.7071067811865487940, 4.178957128135655137E-15 ) ) ;
#214816=CARTESIAN_POINT ( 'NONE',  ( -17.01764560440413376, 66.05000000001224691, -149.2731074837355436 ) ) ;
#214909=CARTESIAN_POINT ( 'NONE',  ( -16.94275863006528482, 66.01050395134471671, -149.1314101024478589 ) ) ;
#214986=CARTESIAN_POINT ( 'NONE',  ( -18.40000000000000213, 64.25000000001230660, -157.3731074845244393 ) ) ;
#215000=( BOUNDED_CURVE ( )  B_SPLINE_CURVE ( 3, ( #32095, #167756, #228996, #146856 ),
 .UNSPECIFIED., .F., .T. ) 
 B_SPLINE_CURVE_WITH_KNOTS ( ( 4, 4 ),
 ( 0.5235987755982449698, 1.570796326794896558 ),
 .UNSPECIFIED. ) 
 CURVE ( )  GEOMETRIC_REPRESENTATION_ITEM ( )  RATIONAL_B_SPLINE_CURVE ( ( 1.000000000000000000, 0.9106836025229499976, 0.9106836025229499976, 1.000000000000000000 ) ) 
 REPRESENTATION_ITEM ( '' )  );
#215098=EDGE_CURVE ( 'NONE', #244466, #90118, #57198, .T. ) ;
#215186=DIRECTION ( 'NONE',  ( -0.000000000000000000, -6.982962677686266711E-15, 1.000000000000000000 ) ) ;
#215200=AXIS2_PLACEMENT_3D ( 'NONE', #82291, #4065, #124030 ) ;
#215267=CARTESIAN_POINT ( 'NONE',  ( 12.93225390519044637, 66.58234804117128647, -154.6643200920840400 ) ) ;
#215353=ORIENTED_EDGE ( 'NONE', *, *, #150017, .F. ) ;
#215608=VERTEX_POINT ( 'NONE', #203802 ) ;
#215723=VERTEX_POINT ( 'NONE', #14620 ) ;
#215725=DIRECTION ( 'NONE',  ( -0.000000000000000000, -6.982962677686266711E-15, 1.000000000000000000 ) ) ;
#215761=ADVANCED_FACE ( 'NONE', ( #15911 ), #96661, .T. ) ;
#215913=ADVANCED_FACE ( 'NONE', ( #231939 ), #205934, .F. ) ;
#215940=ORIENTED_EDGE ( 'NONE', *, *, #148070, .F. ) ;
#216098=EDGE_CURVE ( 'NONE', #196307, #232013, #227026, .T. ) ;
#216180=CARTESIAN_POINT ( 'NONE',  ( -16.90128866880176872, 66.04620422280927983, -149.1604313011357874 ) ) ;
#216240=CARTESIAN_POINT ( 'NONE',  ( -16.87036670365549895, 66.01058118071065905, -157.5026676018264880 ) ) ;
#216545=CARTESIAN_POINT ( 'NONE',  ( 14.22821877134046886, 66.54397173950437150, -155.0119094494586989 ) ) ;
#216547=CARTESIAN_POINT ( 'NONE',  ( -18.40000000000000213, 64.51332499825454647, -145.7731074845244450 ) ) ;
#216575=AXIS2_PLACEMENT_3D ( 'NONE', #77768, #199023, #58203 ) ;
#216893=CIRCLE ( 'NONE', #46024, 0.9000000000000014655 ) ;
#217153=CYLINDRICAL_SURFACE ( 'NONE', #157302, 0.1000000000000038219 ) ;
#217275=ADVANCED_FACE ( 'NONE', ( #73939 ), #153498, .T. ) ;
#217369=CARTESIAN_POINT ( 'NONE',  ( -17.04295772865470937, 65.97510057475071221, -149.1731074845244507 ) ) ;
#217589=CARTESIAN_POINT ( 'NONE',  ( -16.86420534634261514, 66.02938455442051691, -149.1047709352870356 ) ) ;
#217749=CARTESIAN_POINT ( 'NONE',  ( 23.24999999999999645, 67.17743825834588733, -157.3731074845244109 ) ) ;
#217877=DIRECTION ( 'NONE',  ( -1.000000000000000000, -0.000000000000000000, -0.000000000000000000 ) ) ;
#218041=FACE_BOUND ( 'NONE', #112497, .T. ) ;
#218087=ORIENTED_EDGE ( 'NONE', *, *, #30381, .F. ) ;
#218112=CARTESIAN_POINT ( 'NONE',  ( -20.65000000000000568, 68.75000000001226397, -149.1731074845244223 ) ) ;
#218424=CARTESIAN_POINT ( 'NONE',  ( 18.54999999999999716, 67.25000000001229239, -160.7731074845244166 ) ) ;
#218464=DIRECTION ( 'NONE',  ( 0.000000000000000000, -6.982962677686266711E-15, 1.000000000000000000 ) ) ;
#218526=VECTOR ( 'NONE', #217877, 1000.000000000000000 ) ;
#218699=CIRCLE ( 'NONE', #256238, 0.09999999999999105438 ) ;
#218914=CARTESIAN_POINT ( 'NONE',  ( -16.94389599338511943, 66.00880201025724148, -157.4154626827142067 ) ) ;
#219176=ORIENTED_EDGE ( 'NONE', *, *, #121162, .F. ) ;
#219307=CARTESIAN_POINT ( 'NONE',  ( 18.39999999999999503, 64.25000000001224976, -149.1731074845244507 ) ) ;
#219339=CYLINDRICAL_SURFACE ( 'NONE', #226148, 14.30833333333333890 ) ;
#219589=CARTESIAN_POINT ( 'NONE',  ( -16.84419801905645286, 66.05000000001223270, -149.1925973307465085 ) ) ;
#219914=ORIENTED_EDGE ( 'NONE', *, *, #44734, .T. ) ;
#219995=AXIS2_PLACEMENT_3D ( 'NONE', #224563, #9370, #45937 ) ;
#220255=VERTEX_POINT ( 'NONE', #38137 ) ;
#220371=LINE ( 'NONE', #59976, #3425 ) ;
#220425=DIRECTION ( 'NONE',  ( -1.000000000000000000, 0.000000000000000000, -0.000000000000000000 ) ) ;
#220564=CIRCLE ( 'NONE', #4073, 0.09999999999999105438 ) ;
#220680=CARTESIAN_POINT ( 'NONE',  ( -16.87683809663753109, 66.13508622147386973, -156.7473918488857692 ) ) ;
#220917=CARTESIAN_POINT ( 'NONE',  ( -13.11924609551134502, 66.56831044948815190, -151.7438174522883401 ) ) ;
#221159=DIRECTION ( 'NONE',  ( 1.000000000000000000, -1.186688945009010077E-16, -8.286604613020808509E-31 ) ) ;
#221482=CARTESIAN_POINT ( 'NONE',  ( -21.64999999999999858, 65.95000000001225260, -149.1731074845244223 ) ) ;
#221736=ORIENTED_EDGE ( 'NONE', *, *, #117642, .T. ) ;
#221781=VERTEX_POINT ( 'NONE', #217749 ) ;
#221889=EDGE_CURVE ( 'NONE', #2008, #80528, #185061, .T. ) ;
#222012=EDGE_LOOP ( 'NONE', ( #93510, #181900, #163732, #165602, #15476, #174736, #4168, #191151, #196057 ) ) ;
#222102=CARTESIAN_POINT ( 'NONE',  ( -16.93302609847409457, 66.00331747920908754, -157.4367189891619034 ) ) ;
#222171=EDGE_CURVE ( 'NONE', #45933, #48358, #251453, .T. ) ;
#222189=CARTESIAN_POINT ( 'NONE',  ( -14.56336952470178758, 66.55335465531700834, -151.6123010284242127 ) ) ;
#222555=FACE_OUTER_BOUND ( 'NONE', #165841, .T. ) ;
#222558=VERTEX_POINT ( 'NONE', #109056 ) ;
#222575=CARTESIAN_POINT ( 'NONE',  ( 21.72449340488909897, 65.71604372252112114, -149.1731074845244507 ) ) ;
#222650=B_SPLINE_CURVE_WITH_KNOTS ( 'NONE', 3,
 ( #81947, #203214, #119858, #100234, #3729, #102806, #139369, #141952, #218914, #1142 ),
 .UNSPECIFIED., .F., .F.,
 ( 4, 3, 3, 4 ),
 ( 1.883833020489685736E-15, 3.877043166999269576E-05, 7.336897548476537185E-05, 7.659383120240726740E-05 ),
 .UNSPECIFIED. ) ;
#222900=FACE_OUTER_BOUND ( 'NONE', #199614, .T. ) ;
#222939=EDGE_CURVE ( 'NONE', #67174, #230022, #82741, .T. ) ;
#222965=CARTESIAN_POINT ( 'NONE',  ( -18.40000000000000213, 70.35000000001230092, -157.3731074845244109 ) ) ;
#223321=CARTESIAN_POINT ( 'NONE',  ( 20.27550659511089037, 66.78395627750339258, -149.1731074845244223 ) ) ;
#223437=FACE_OUTER_BOUND ( 'NONE', #223730, .T. ) ;
#223457=CIRCLE ( 'NONE', #156878, 14.20833333333333748 ) ;
#223471=AXIS2_PLACEMENT_3D ( 'NONE', #247468, #45420, #243616 ) ;
#223730=EDGE_LOOP ( 'NONE', ( #23067, #249103, #80938, #92074, #45660 ) ) ;
#223862=CARTESIAN_POINT ( 'NONE',  ( -16.87683809663752754, 66.13411015068081156, -156.7556806774549045 ) ) ;
#223907=FACE_OUTER_BOUND ( 'NONE', #86787, .T. ) ;
#223920=CARTESIAN_POINT ( 'NONE',  ( -18.39999999999999858, 64.52683809664983983, -160.6971614177164724 ) ) ;
#224488=( BOUNDED_SURFACE ( )  B_SPLINE_SURFACE ( 3, 2, ( 
 ( #27451, #69118, #249037 ),
 ( #251585, #72984, #228181 ),
 ( #230758, #190350, #109494 ),
 ( #189049, #70422, #229464 ) ),
 .UNSPECIFIED., .F., .F., .F. ) 
 B_SPLINE_SURFACE_WITH_KNOTS ( ( 4, 4 ),
 ( 3, 3 ),
 ( 0.0008258556059633768206, 0.0009616864997632988948 ),
 ( 0.000000000000000000, 1.000000000000000000 ),
 .UNSPECIFIED. ) 
 GEOMETRIC_REPRESENTATION_ITEM ( )  RATIONAL_B_SPLINE_SURFACE ( (
 ( 1.000000000000000000, 0.9152888060719485130, 1.000000000000000000),
 ( 1.000000000000000000, 0.9327727094137853170, 1.000000000000000000),
 ( 1.000000000000000000, 0.9369023509258459503, 1.000000000000000000),
 ( 1.000000000000000000, 0.9246339933864583527, 1.000000000000000000) ) ) 
 REPRESENTATION_ITEM ( '' )  SURFACE ( )  );
#224550=ORIENTED_EDGE ( 'NONE', *, *, #34144, .F. ) ;
#224563=CARTESIAN_POINT ( 'NONE',  ( 20.99999999999999645, 66.25000000001230660, -157.3731074845244393 ) ) ;
#224685=CARTESIAN_POINT ( 'NONE',  ( -16.94037747912386394, 65.98646061752597802, -157.4719765265489286 ) ) ;
#224767=DIRECTION ( 'NONE',  ( 1.000000000000000000, 0.000000000000000000, 0.000000000000000000 ) ) ;
#224786=VERTEX_POINT ( 'NONE', #64914 ) ;
#224905=DIRECTION ( 'NONE',  ( -0.000000000000000000, -6.982962677686266711E-15, 1.000000000000000000 ) ) ;
#224966=FACE_OUTER_BOUND ( 'NONE', #1623, .T. ) ;
#225209=CARTESIAN_POINT ( 'NONE',  ( -14.87779219673431363, 66.56936653093950440, -154.7913416897003742 ) ) ;
#225374=CARTESIAN_POINT ( 'NONE',  ( -17.11825945287482753, 66.05000000001231797, -157.2731074845244166 ) ) ;
#225539=VERTEX_POINT ( 'NONE', #129110 ) ;
#225624=ORIENTED_EDGE ( 'NONE', *, *, #45027, .T. ) ;
#225923=CARTESIAN_POINT ( 'NONE',  ( -20.65000000000000568, 70.35000000001230092, -157.3731074845244109 ) ) ;
#226148=AXIS2_PLACEMENT_3D ( 'NONE', #57691, #120292, #201069 ) ;
#226303=CARTESIAN_POINT ( 'NONE',  ( -18.40000000000000213, 64.52683809664981140, -157.4731074845244621 ) ) ;
#226322=DIRECTION ( 'NONE',  ( 1.000000000000000000, 0.000000000000000000, 0.000000000000000000 ) ) ;
#226423=CARTESIAN_POINT ( 'NONE',  ( -16.80891096016298647, 66.05000000001230376, -157.3907702917945812 ) ) ;
#226492=CARTESIAN_POINT ( 'NONE',  ( -12.60206096961793598, 66.61031399435663047, -154.3502639781731318 ) ) ;
#226609=B_SPLINE_CURVE_WITH_KNOTS ( 'NONE', 3,
 ( #56171, #138273, #97850, #118751, #96575, #176163, #215267, #36662, #116185, #195731, #255622, #77028, #236110, #137010, #216545, #170615, #191440, #192695, #51869, #151002, #173177, #131423, #96132, #50588, #195280, #248823 ),
 .UNSPECIFIED., .F., .F.,
 ( 4, 2, 2, 2, 2, 2, 2, 2, 2, 2, 2, 2, 4 ),
 ( 0.005476422646581303143, 0.006160811967703536639, 0.006845201288825770135, 0.007187395949386886883, 0.007529590609948002763, 0.007871785270509119511, 0.008213979931070236259, 0.008556174591631353007, 0.008898369252192471490, 0.009240563912753588238, 0.009582758573314703252, 0.01026714789443687430, 0.01095153721555904534 ),
 .UNSPECIFIED. ) ;
#227004=AXIS2_PLACEMENT_3D ( 'NONE', #29110, #47317, #186872 ) ;
#227026=B_SPLINE_CURVE_WITH_KNOTS ( 'NONE', 3,
 ( #165261, #205656, #105243, #25754, #81833, #6176, #85684, #225209, #46578, #143112, #103976, #62315, #161435, #183551, #33498, #51702, #8761, #229093, #146964, #68736, #170451, #226492, #129964, #128713, #86978, #247356 ),
 .UNSPECIFIED., .F., .F.,
 ( 4, 2, 2, 2, 2, 2, 2, 2, 2, 2, 2, 2, 4 ),
 ( 0.005476422646581329164, 0.006160811967703599956, 0.006845201288825871616, 0.007187395949386978823, 0.007529590609948086030, 0.007871785270509192370, 0.008213979931070300444, 0.008556174591631406784, 0.008898369252192513124, 0.009240563912753619463, 0.009582758573314727538, 0.01026714789443688644, 0.01095153721555904361 ),
 .UNSPECIFIED. ) ;
#227164=ORIENTED_EDGE ( 'NONE', *, *, #194776, .T. ) ;
#227424=CARTESIAN_POINT ( 'NONE',  ( -16.87683809663752399, 66.05000000001230376, -157.3731074845244393 ) ) ;
#227482=CARTESIAN_POINT ( 'NONE',  ( 20.73486653747090003, 68.75000000001222134, -149.1731074845244223 ) ) ;
#227858=CARTESIAN_POINT ( 'NONE',  ( -16.88593481969334320, 66.04943990992792635, -149.1712352275798992 ) ) ;
#227964=FACE_OUTER_BOUND ( 'NONE', #45935, .T. ) ;
#227977=AXIS2_PLACEMENT_3D ( 'NONE', #44252, #126341, #48086 ) ;
#227999=VERTEX_POINT ( 'NONE', #223321 ) ;
#228044=ORIENTED_EDGE ( 'NONE', *, *, #229237, .T. ) ;
#228063=ORIENTED_EDGE ( 'NONE', *, *, #68785, .F. ) ;
#228181=CARTESIAN_POINT ( 'NONE',  ( -16.92778301347287950, 65.99905508317688430, -149.0945893765574510 ) ) ;
#228262=DIRECTION ( 'NONE',  ( -1.000000000000000000, 0.000000000000000000, 0.000000000000000000 ) ) ;
#228384=ORIENTED_EDGE ( 'NONE', *, *, #207080, .F. ) ;
#228440=ORIENTED_EDGE ( 'NONE', *, *, #215098, .T. ) ;
#228918=CARTESIAN_POINT ( 'NONE',  ( 20.27550659511088682, 66.78395627750346364, -160.7731074845244166 ) ) ;
#228996=CARTESIAN_POINT ( 'NONE',  ( -17.01473183483381391, 66.05000000001230376, -157.2731074845244166 ) ) ;
#229033=CARTESIAN_POINT ( 'NONE',  ( -16.78569801330234057, 66.05206626689880522, -157.3661945791769199 ) ) ;
#229045=DIRECTION ( 'NONE',  ( 1.186688945009009831E-16, 1.000000000000000000, 6.982962677686266711E-15 ) ) ;
#229093=CARTESIAN_POINT ( 'NONE',  ( -13.22483237240080278, 66.56332574816946135, -154.8462455535252786 ) ) ;
#229206=AXIS2_PLACEMENT_3D ( 'NONE', #61461, #159295, #22358 ) ;
#229209=EDGE_LOOP ( 'NONE', ( #110720, #130313, #46270, #9548 ) ) ;
#229237=EDGE_CURVE ( 'NONE', #127923, #257588, #210251, .T. ) ;
#229421=VECTOR ( 'NONE', #109986, 1000.000000000000000 ) ;
#229464=CARTESIAN_POINT ( 'NONE',  ( -16.94878442675510399, 66.00827089702124795, -149.1348879088865829 ) ) ;
#229657=CARTESIAN_POINT ( 'NONE',  ( 15.73863059295127798, 66.64859682587062650, -153.0435770476859147 ) ) ;
#229690=ORIENTED_EDGE ( 'NONE', *, *, #126595, .F. ) ;
#229781=AXIS2_PLACEMENT_3D ( 'NONE', #239209, #224767, #200089 ) ;
#229794=CARTESIAN_POINT ( 'NONE',  ( -16.87331047859651179, 66.05000000001230376, -157.3731074845244393 ) ) ;
#230022=VERTEX_POINT ( 'NONE', #179810 ) ;
#230151=ORIENTED_EDGE ( 'NONE', *, *, #132721, .F. ) ;
#230262=LINE ( 'NONE', #110320, #170607 ) ;
#230269=VERTEX_POINT ( 'NONE', #17502 ) ;
#230382=B_SPLINE_CURVE_WITH_KNOTS ( 'NONE', 3,
 ( #236267, #197130, #91624, #171210 ),
 .UNSPECIFIED., .F., .F.,
 ( 4, 4 ),
 ( 0.000000000000000000, 7.713889350930586977E-05 ),
 .UNSPECIFIED. ) ;
#230436=EDGE_CURVE ( 'NONE', #47223, #90118, #118455, .T. ) ;
#230758=CARTESIAN_POINT ( 'NONE',  ( -16.86445178670593492, 66.03778837089635090, -149.1323300464075601 ) ) ;
#230809=DIRECTION ( 'NONE',  ( 1.186688945009010077E-16, 1.000000000000000000, 6.982962677686266711E-15 ) ) ;
#230819=EDGE_CURVE ( 'NONE', #3667, #128197, #52871, .T. ) ;
#230907=CARTESIAN_POINT ( 'NONE',  ( -18.40000000000000213, 64.52683809664972614, -145.8490535513323891 ) ) ;
#230953=CARTESIAN_POINT ( 'NONE',  ( -16.80070461187849773, 66.05000000001224691, -149.1700713136813761 ) ) ;
#230996=EDGE_CURVE ( 'NONE', #46648, #164969, #176248, .T. ) ;
#231107=CARTESIAN_POINT ( 'NONE',  ( -16.87487986503753845, 66.04999244492670130, -157.3731327448377044 ) ) ;
#231357=CARTESIAN_POINT ( 'NONE',  ( 18.39999999999997371, 64.25000000001233502, -160.7731074845244450 ) ) ;
#231411=ORIENTED_EDGE ( 'NONE', *, *, #27545, .F. ) ;
#231571=CARTESIAN_POINT ( 'NONE',  ( -16.77683809663752257, 66.05000000001224691, -149.1731074845244223 ) ) ;
#231638=ORIENTED_EDGE ( 'NONE', *, *, #208566, .F. ) ;
#231703=ORIENTED_EDGE ( 'NONE', *, *, #208905, .F. ) ;
#231839=CARTESIAN_POINT ( 'NONE',  ( -16.87242674293849021, 66.05000000001224691, -149.1720172381520797 ) ) ;
#231901=VECTOR ( 'NONE', #73415, 1000.000000000000000 ) ;
#231939=FACE_OUTER_BOUND ( 'NONE', #45801, .T. ) ;
#232013=VERTEX_POINT ( 'NONE', #257036 ) ;
#232094=VERTEX_POINT ( 'NONE', #61455 ) ;
#232128=CARTESIAN_POINT ( 'NONE',  ( -21.64999999999999858, 65.95000000001230944, -157.2731074845244166 ) ) ;
#232206=DIRECTION ( 'NONE',  ( 0.000000000000000000, -0.9553114395363127009, 0.2956011730204364252 ) ) ;
#232483=VECTOR ( 'NONE', #253965, 1000.000000000000000 ) ;
#232710=EDGE_CURVE ( 'NONE', #122105, #16882, #80365, .T. ) ;
#232745=CARTESIAN_POINT ( 'NONE',  ( 23.24999999999999645, 64.25000000001233502, -160.7731074845244450 ) ) ;
#232778=DIRECTION ( 'NONE',  ( 1.000000000000000000, -7.125593699324843413E-30, 1.020425574104004196E-15 ) ) ;
#232788=CARTESIAN_POINT ( 'NONE',  ( -18.44085059012131822, 64.48598750652851663, -160.7634128036459913 ) ) ;
#232900=CARTESIAN_POINT ( 'NONE',  ( -16.77828822508139694, 66.05377062509154484, -157.3604792331504711 ) ) ;
#233136=CARTESIAN_POINT ( 'NONE',  ( -17.11825945287481687, 66.05000000001224691, -149.1731074845244507 ) ) ;
#233514=CARTESIAN_POINT ( 'NONE',  ( -16.97683810757273193, 66.05000000001224691, -149.7866841969855614 ) ) ;
#233548=PLANE ( 'NONE',  #71282 ) ;
#233590=EDGE_LOOP ( 'NONE', ( #238309, #246500 ) ) ;
#233602=ORIENTED_EDGE ( 'NONE', *, *, #26632, .F. ) ;
#233668=EDGE_CURVE ( 'NONE', #184435, #32558, #100108, .T. ) ;
#233808=EDGE_LOOP ( 'NONE', ( #145744, #156359, #134337, #218087, #79446, #168652, #26401, #174831, #164264, #85918 ) ) ;
#233832=LINE ( 'NONE', #254639, #131541 ) ;
#233928=EDGE_LOOP ( 'NONE', ( #33165, #53441, #136434, #193933, #76492, #151908, #57939, #1540, #76046, #206492, #172157, #166938, #140583, #145806 ) ) ;
#233941=VECTOR ( 'NONE', #177011, 1000.000000000000000 ) ;
#234182=CARTESIAN_POINT ( 'NONE',  ( -23.25000000000000355, 66.05000000001233218, -160.7731074845244166 ) ) ;
#234220=LINE ( 'NONE', #195136, #163101 ) ;
#234372=LINE ( 'NONE', #257738, #233941 ) ;
#234375=CARTESIAN_POINT ( 'NONE',  ( -17.05016517655717578, 66.05000000001224691, -149.1958054805180325 ) ) ;
#234446=CARTESIAN_POINT ( 'NONE',  ( -20.65000000000000568, 68.75000000001226397, -149.1731074845244223 ) ) ;
#234488=VECTOR ( 'NONE', #44540, 1000.000000000000000 ) ;
#234745=CARTESIAN_POINT ( 'NONE',  ( -17.22767730082145832, 65.65075578754345997, -147.8806787939494143 ) ) ;
#234756=EDGE_CURVE ( 'NONE', #42338, #53868, #89793, .T. ) ;
#234778=FACE_OUTER_BOUND ( 'NONE', #183066, .T. ) ;
#234922=DIRECTION ( 'NONE',  ( 1.000000000000000000, 0.000000000000000000, 0.000000000000000000 ) ) ;
#234928=ORIENTED_EDGE ( 'NONE', *, *, #60521, .T. ) ;
#235281=EDGE_CURVE ( 'NONE', #48358, #56214, #179034, .T. ) ;
#235288=( NAMED_UNIT ( * ) PLANE_ANGLE_UNIT ( ) SI_UNIT ( $, .RADIAN. ) );
#235360=ORIENTED_EDGE ( 'NONE', *, *, #121323, .F. ) ;
#235445=EDGE_CURVE ( 'NONE', #107287, #184435, #169740, .T. ) ;
#235459=VERTEX_POINT ( 'NONE', #111009 ) ;
#235542=ORIENTED_EDGE ( 'NONE', *, *, #195, .F. ) ;
#235811=CARTESIAN_POINT ( 'NONE',  ( -16.86337532320261801, 66.02003279578794093, -157.4720319535072406 ) ) ;
#235868=VECTOR ( 'NONE', #248446, 1000.000000000000000 ) ;
#236023=CARTESIAN_POINT ( 'NONE',  ( -18.44085059012132177, 64.48598750652841716, -145.7828021654028987 ) ) ;
#236030=CARTESIAN_POINT ( 'NONE',  ( 20.05000000000002913, 68.75000000001230660, -160.7731074845244166 ) ) ;
#236053=CARTESIAN_POINT ( 'NONE',  ( -16.94107738177415712, 65.98576071487568129, -157.4731074845244336 ) ) ;
#236073=FACE_OUTER_BOUND ( 'NONE', #182698, .T. ) ;
#236110=CARTESIAN_POINT ( 'NONE',  ( 13.88302573338719803, 66.54258905524487488, -155.0230235107344470 ) ) ;
#236218=CARTESIAN_POINT ( 'NONE',  ( -16.80469485234340965, 66.05784833687121704, -149.2131406405932808 ) ) ;
#236264=VECTOR ( 'NONE', #123994, 1000.000000000000000 ) ;
#236267=CARTESIAN_POINT ( 'NONE',  ( -18.39999999999999858, 64.52683809664983983, -160.6971614177164724 ) ) ;
#236554=AXIS2_PLACEMENT_3D ( 'NONE', #32842, #249293, #51038 ) ;
#236636=VECTOR ( 'NONE', #251025, 999.9999999999998863 ) ;
#236702=PLANE ( 'NONE',  #183714 ) ;
#236724=FACE_OUTER_BOUND ( 'NONE', #72734, .T. ) ;
#236813=CARTESIAN_POINT ( 'NONE',  ( -16.87683809663752399, 52.34166666667894674, -153.2731074845245303 ) ) ;
#237039=EDGE_LOOP ( 'NONE', ( #22384, #51716, #56817, #114273 ) ) ;
#237518=CARTESIAN_POINT ( 'NONE',  ( -16.87372397896795562, 66.11940046337051058, -149.6723829744886416 ) ) ;
#237736=ORIENTED_EDGE ( 'NONE', *, *, #208341, .F. ) ;
#237829=CARTESIAN_POINT ( 'NONE',  ( -16.92973740335397181, 66.00749618554532105, -157.4291665197260102 ) ) ;
#237858=MECHANICAL_DESIGN_GEOMETRIC_PRESENTATION_REPRESENTATION('',(#62894),#138071);
#237925=CARTESIAN_POINT ( 'NONE',  ( -12.60829076262180060, 66.61047060254553287, -152.2059995716306844 ) ) ;
#237936=CARTESIAN_POINT ( 'NONE',  ( -18.34804628011471195, 64.52683809664993930, -160.7731074845244450 ) ) ;
#237999=FACE_OUTER_BOUND ( 'NONE', #71130, .T. ) ;
#238030=CARTESIAN_POINT ( 'NONE',  ( -16.93826681692523195, 65.98857127972452474, -149.0776490171649868 ) ) ;
#238031=ORIENTED_EDGE ( 'NONE', *, *, #56966, .F. ) ;
#238054=CARTESIAN_POINT ( 'NONE',  ( -21.65000000000000213, 66.05000000001230376, -157.3731074845244393 ) ) ;
#238280=DIRECTION ( 'NONE',  ( 1.000000000000000000, 0.000000000000000000, 0.000000000000000000 ) ) ;
#238309=ORIENTED_EDGE ( 'NONE', *, *, #60183, .T. ) ;
#238447=VERTEX_POINT ( 'NONE', #55081 ) ;
#238963=ORIENTED_EDGE ( 'NONE', *, *, #257460, .F. ) ;
#238966=CARTESIAN_POINT ( 'NONE',  ( -16.83199030136657726, 66.06935196689877898, -157.2507064618668835 ) ) ;
#239170=CARTESIAN_POINT ( 'NONE',  ( -16.86133551771148831, 66.05000000001224691, -149.2217640499777929 ) ) ;
#239209=CARTESIAN_POINT ( 'NONE',  ( -17.11825945287482753, 65.95000000001230944, -157.2731074845244166 ) ) ;
#239324=AXIS2_PLACEMENT_3D ( 'NONE', #79015, #157337, #59441 ) ;
#239330=CARTESIAN_POINT ( 'NONE',  ( -16.93211319090181632, 66.00001321885476102, -149.1006019852513589 ) ) ;
#239521=DIRECTION ( 'NONE',  ( -1.000000000000000000, 0.000000000000000000, 0.000000000000000000 ) ) ;
#239579=LINE ( 'NONE', #240863, #35626 ) ;
#239763=EDGE_LOOP ( 'NONE', ( #49844, #45140, #73693, #130944 ) ) ;
#239808=CARTESIAN_POINT ( 'NONE',  ( -18.40000000000000213, 64.52683809664981140, -157.3731074845244393 ) ) ;
#239874=EDGE_LOOP ( 'NONE', ( #30671, #41863, #30114, #43554 ) ) ;
#240031=VERTEX_POINT ( 'NONE', #134364 ) ;
#240655=ORIENTED_EDGE ( 'NONE', *, *, #115170, .T. ) ;
#240829=CARTESIAN_POINT ( 'NONE',  ( -16.87036670365548474, 66.01058118071060221, -149.0435473672224020 ) ) ;
#240863=CARTESIAN_POINT ( 'NONE',  ( 18.54999999999999716, 67.25000000001222134, -149.1731074845244223 ) ) ;
#240915=EDGE_LOOP ( 'NONE', ( #152246, #123830, #121511, #248226 ) ) ;
#240932=PLANE ( 'NONE',  #4958 ) ;
#240964=DIRECTION ( 'NONE',  ( 0.000000000000000000, 6.982962677686266711E-15, -1.000000000000000000 ) ) ;
#241397=CARTESIAN_POINT ( 'NONE',  ( -17.11825945287482753, 65.95000000001232365, -157.3731074845244393 ) ) ;
#241605=VECTOR ( 'NONE', #196268, 1000.000000000000000 ) ;
#241738=DIRECTION ( 'NONE',  ( 0.000000000000000000, 0.9553114395363127009, 0.2956011730204364252 ) ) ;
#241777=CARTESIAN_POINT ( 'NONE',  ( -12.25000000000000178, 66.65000000001228386, -153.2731074845244166 ) ) ;
#241942=VECTOR ( 'NONE', #49749, 1000.000000000000000 ) ;
#241983=CARTESIAN_POINT ( 'NONE',  ( 13.99999999999999822, 66.15000000001228386, -153.2731074845244450 ) ) ;
#242079=LINE ( 'NONE', #63439, #35765 ) ;
#242275=EDGE_CURVE ( 'NONE', #22326, #90118, #220564, .T. ) ;
#242305=CARTESIAN_POINT ( 'NONE',  ( -16.87304349924914604, 66.03825492205506009, -149.1340408094791599 ) ) ;
#242400=EDGE_CURVE ( 'NONE', #151632, #47244, #160378, .T. ) ;
#242402=SURFACE_STYLE_USAGE ( .BOTH. , #162906 ) ;
#242616=DIRECTION ( 'NONE',  ( -1.020425574104004196E-15, 6.982962677686266711E-15, -1.000000000000000000 ) ) ;
#242652=FACE_OUTER_BOUND ( 'NONE', #206277, .T. ) ;
#242721=EDGE_CURVE ( 'NONE', #250417, #4697, #33722, .T. ) ;
#242743=DIRECTION ( 'NONE',  ( 0.000000000000000000, -1.000000000000000000, -6.982962677686266711E-15 ) ) ;
#243060=CARTESIAN_POINT ( 'NONE',  ( -15.51798037960204546, 66.62334006147872856, -152.3949149363072024 ) ) ;
#243239=CIRCLE ( 'NONE', #201549, 0.09999999999998898659 ) ;
#243501=CARTESIAN_POINT ( 'NONE',  ( -17.78043020864321022, 65.14640788800663529, -159.6861566502446124 ) ) ;
#243507=CIRCLE ( 'NONE', #210216, 1.500000000000001332 ) ;
#243616=DIRECTION ( 'NONE',  ( 0.000000000000000000, 6.982962677686266711E-15, -1.000000000000000000 ) ) ;
#243778=AXIS2_PLACEMENT_3D ( 'NONE', #166930, #209883, #31275 ) ;
#244150=EDGE_LOOP ( 'NONE', ( #140789, #191625, #191468 ) ) ;
#244248=CARTESIAN_POINT ( 'NONE',  ( 18.39999999999999503, 64.52683809664974035, -149.1731074845244507 ) ) ;
#244466=VERTEX_POINT ( 'NONE', #114222 ) ;
#244623=EDGE_LOOP ( 'NONE', ( #238031, #32267, #228384, #159094 ) ) ;
#244631=ORIENTED_EDGE ( 'NONE', *, *, #242721, .T. ) ;
#244712=CARTESIAN_POINT ( 'NONE',  ( -16.80070461187834496, 66.05000000001230376, -157.3761436553679118 ) ) ;
#244794=DIRECTION ( 'NONE',  ( 0.000000000000000000, 0.000000000000000000, -1.000000000000000000 ) ) ;
#244891=CARTESIAN_POINT ( 'NONE',  ( -16.97683809663752186, 66.15000000001225544, -149.9254715027207396 ) ) ;
#245060=CARTESIAN_POINT ( 'NONE',  ( 20.73486653747088582, 68.75000000001227818, -157.3731074845244109 ) ) ;
#245403=B_SPLINE_CURVE_WITH_KNOTS ( 'NONE', 3,
 ( #241777, #141390, #177972, #38445, #60563, #158429, #102228, #237925, #140092, #63128, #220917, #24042, #42302, #43588, #181810, #142659, #222189, #202649, #103537, #183108, #128266, #83941, #25329, #243060, #66998, #163532, #89129, #48709, #69587, #149126 ),
 .UNSPECIFIED., .F., .F.,
 ( 4, 2, 2, 2, 2, 2, 2, 2, 2, 2, 2, 2, 2, 2, 4 ),
 ( 0.000000000000000000, 0.0003422764154113113887, 0.0006845528308226227774, 0.001026829246233934220, 0.001369105661645245555, 0.002053658492467929590, 0.002738211323290614275, 0.003080487738701953148, 0.003422764154113292889, 0.003765040569524632195, 0.004107316984935971069, 0.004449593400347310809, 0.004791869815758650550, 0.005134146231169990290, 0.005476422646581329164 ),
 .UNSPECIFIED. ) ;
#245579=EDGE_CURVE ( 'NONE', #240031, #18265, #230382, .T. ) ;
#245763=ORIENTED_EDGE ( 'NONE', *, *, #192474, .F. ) ;
#245922=CYLINDRICAL_SURFACE ( 'NONE', #169925, 1.749999999999998002 ) ;
#246036=EDGE_CURVE ( 'NONE', #17339, #45933, #110883, .T. ) ;
#246359=CARTESIAN_POINT ( 'NONE',  ( -23.25000000000000355, 64.25000000001224976, -149.1731074845244507 ) ) ;
#246384=ORIENTED_EDGE ( 'NONE', *, *, #230819, .F. ) ;
#246500=ORIENTED_EDGE ( 'NONE', *, *, #56966, .T. ) ;
#246516=ORIENTED_EDGE ( 'NONE', *, *, #213629, .F. ) ;
#246620=PLANE ( 'NONE',  #124502 ) ;
#246638=( BOUNDED_SURFACE ( )  B_SPLINE_SURFACE ( 3, 2, ( 
 ( #231839, #12802, #153622 ),
 ( #55704, #193996, #136549 ),
 ( #214816, #234375, #217369 ),
 ( #17893, #233136, #53181 ) ),
 .UNSPECIFIED., .F., .F., .F. ) 
 B_SPLINE_SURFACE_WITH_KNOTS ( ( 4, 4 ),
 ( 3, 3 ),
 ( 3.658908243880847788, 4.712388980384689674 ),
 ( 0.000000000000000000, 1.000000000000000000 ),
 .UNSPECIFIED. ) 
 GEOMETRIC_REPRESENTATION_ITEM ( )  RATIONAL_B_SPLINE_SURFACE ( (
 ( 1.000000000000000000, 0.8984936768950640973, 1.000000000000000000),
 ( 1.000000000000000000, 0.8646876308616029405, 1.000000000000000000),
 ( 1.000000000000000000, 0.7953136715913016186, 1.000000000000000000),
 ( 1.000000000000000000, 0.7071067811865475727, 1.000000000000000000) ) ) 
 REPRESENTATION_ITEM ( '' )  SURFACE ( )  );
#246664=DIRECTION ( 'NONE',  ( 1.000000000000000000, 0.000000000000000000, 0.000000000000000000 ) ) ;
#246673=VERTEX_POINT ( 'NONE', #63419 ) ;
#246684=EDGE_CURVE ( 'NONE', #127923, #58960, #24327, .T. ) ;
#247185=CARTESIAN_POINT ( 'NONE',  ( -16.94107738177415357, 65.98576071487568129, -157.4731074845244621 ) ) ;
#247356=CARTESIAN_POINT ( 'NONE',  ( -12.25000000000000178, 66.65000000001228386, -153.2731074845244166 ) ) ;
#247372=ORIENTED_EDGE ( 'NONE', *, *, #122264, .F. ) ;
#247468=CARTESIAN_POINT ( 'NONE',  ( 16.27683809663750125, 66.65000000001234071, -160.7731074845244166 ) ) ;
#247661=ORIENTED_EDGE ( 'NONE', *, *, #213629, .T. ) ;
#247739=DIRECTION ( 'NONE',  ( -0.000000000000000000, -6.982962677686266711E-15, 1.000000000000000000 ) ) ;
#247923=CARTESIAN_POINT ( 'NONE',  ( 13.22461703343584638, 66.56333706821315843, -151.7000707522295215 ) ) ;
#248158=CARTESIAN_POINT ( 'NONE',  ( -18.40000000000000568, 64.52683809664975456, -149.1316861282871287 ) ) ;
#248195=( BOUNDED_SURFACE ( )  B_SPLINE_SURFACE ( 3, 2, ( 
 ( #182200, #203026, #64802 ),
 ( #83046, #60948, #223862 ),
 ( #24428, #140479, #81767 ),
 ( #45246, #23142, #103907 ),
 ( #124792, #161359, #62245 ),
 ( #29568, #50352, #165195 ),
 ( #188600, #9970, #167791 ),
 ( #7391, #109059, #205585 ),
 ( #226423, #244712, #71250 ),
 ( #204302, #69967, #47790 ) ),
 .UNSPECIFIED., .F., .F., .F. ) 
 B_SPLINE_SURFACE_WITH_KNOTS ( ( 4, 2, 2, 2, 4 ),
 ( 3, 3 ),
 ( 0.002161241639767785133, 0.002579950749617451571, 0.002789305304542284789, 0.002893982582004701182, 0.002998659859467118008 ),
 ( 0.000000000000000000, 1.000000000000000000 ),
 .UNSPECIFIED. ) 
 GEOMETRIC_REPRESENTATION_ITEM ( )  RATIONAL_B_SPLINE_SURFACE ( (
 ( 1.000000000000000000, 0.7071067811864985009, 1.000000000000000000),
 ( 1.000000000000000000, 0.7632447400666292348, 1.000000000000000000),
 ( 1.000000000000000000, 0.8158073005106037945, 1.000000000000000000),
 ( 1.000000000000000000, 0.8906973462397418384, 1.000000000000000000),
 ( 1.000000000000000000, 0.9149408947799445579, 1.000000000000000000),
 ( 1.000000000000000000, 0.9493368785276108390, 1.000000000000000000),
 ( 1.000000000000000000, 0.9605194247158034271, 1.000000000000000000),
 ( 1.000000000000000000, 0.9803630264779761294, 1.000000000000000000),
 ( 1.000000000000000000, 0.9900844824272162503, 1.000000000000000000),
 ( 1.000000000000000000, 0.9894588281429244070, 1.000000000000000000) ) ) 
 REPRESENTATION_ITEM ( '' )  SURFACE ( )  );
#248226=ORIENTED_EDGE ( 'NONE', *, *, #45729, .T. ) ;
#248350=ORIENTED_EDGE ( 'NONE', *, *, #253906, .F. ) ;
#248400=EDGE_CURVE ( 'NONE', #215723, #46648, #132130, .T. ) ;
#248446=DIRECTION ( 'NONE',  ( -0.000000000000000000, -6.982962677686266711E-15, 1.000000000000000000 ) ) ;
#248712=CARTESIAN_POINT ( 'NONE',  ( -16.89081410710458542, 66.04868147016512125, -149.1687015646880639 ) ) ;
#248821=CARTESIAN_POINT ( 'NONE',  ( -16.92209698673622853, 66.05000000001231797, -157.3124719174703898 ) ) ;
#248823=CARTESIAN_POINT ( 'NONE',  ( 15.74999999999999645, 66.65000000001228386, -153.2731074845244166 ) ) ;
#249037=CARTESIAN_POINT ( 'NONE',  ( -16.94107738177414291, 65.98576071487562444, -149.0731074845244279 ) ) ;
#249103=ORIENTED_EDGE ( 'NONE', *, *, #188627, .T. ) ;
#249259=FACE_OUTER_BOUND ( 'NONE', #239874, .T. ) ;
#249293=DIRECTION ( 'NONE',  ( 1.000000000000000000, -1.186688945009010077E-16, -8.286604613020808509E-31 ) ) ;
#249467=LINE ( 'NONE', #70847, #231901 ) ;
#249661=CARTESIAN_POINT ( 'NONE',  ( -33.72168855820451938, 66.05000000001228955, -157.3731074845244962 ) ) ;
#249868=CARTESIAN_POINT ( 'NONE',  ( -16.80438519320023616, 66.05022090354395914, -157.3723692036031423 ) ) ;
#250392=CARTESIAN_POINT ( 'NONE',  ( -20.65000000000000568, 70.35000000001232934, -160.7731074845243882 ) ) ;
#250417=VERTEX_POINT ( 'NONE', #162945 ) ;
#250489=CARTESIAN_POINT ( 'NONE',  ( 13.77030915526558807, 66.54399267394292394, -151.5344739903776485 ) ) ;
#250906=ORIENTED_EDGE ( 'NONE', *, *, #195657, .T. ) ;
#251025=DIRECTION ( 'NONE',  ( 0.5932847527679299127, 0.8049926720990051576, 4.984624513800587583E-15 ) ) ;
#251027=CARTESIAN_POINT ( 'NONE',  ( -17.27223548802716735, 65.65460260865560826, -158.6567136637387705 ) ) ;
#251063=B_SPLINE_CURVE_WITH_KNOTS ( 'NONE', 3,
 ( #98917, #102771, #182353, #242305, #2395, #217589, #140636, #256690, #178518, #21998 ),
 .UNSPECIFIED., .F., .F.,
 ( 4, 3, 3, 4 ),
 ( 7.632826238681267430E-06, 4.756916949875584252E-05, 9.484459048148792613E-05, 0.0001435500935099677739 ),
 .UNSPECIFIED. ) ;
#251429=ORIENTED_EDGE ( 'NONE', *, *, #31224, .F. ) ;
#251453=LINE ( 'NONE', #234446, #91099 ) ;
#251495=CARTESIAN_POINT ( 'NONE',  ( 16.87683809663749557, 66.05000000001226113, -149.1731074845244223 ) ) ;
#251500=VERTEX_POINT ( 'NONE', #36633 ) ;
#251585=CARTESIAN_POINT ( 'NONE',  ( -16.85718274719422283, 66.02385768539039645, -149.0864538167066371 ) ) ;
#251745=CARTESIAN_POINT ( 'NONE',  ( -16.87036670365549895, 65.91505003675702312, -157.4731074845244336 ) ) ;
#251772=CARTESIAN_POINT ( 'NONE',  ( -16.83558968593874994, 66.05000000001224691, -149.1854126721411262 ) ) ;
#251775=CARTESIAN_POINT ( 'NONE',  ( -18.40000000000000213, 67.17743825834580207, -145.7731074845244450 ) ) ;
#252055=ORIENTED_EDGE ( 'NONE', *, *, #88654, .T. ) ;
#252314=CARTESIAN_POINT ( 'NONE',  ( 18.39999999999998082, 64.52683809664983983, -160.7731074845244450 ) ) ;
#252649=VERTEX_POINT ( 'NONE', #143616 ) ;
#252783=AXIS2_PLACEMENT_3D ( 'NONE', #122299, #197004, #240964 ) ;
#253006=CARTESIAN_POINT ( 'NONE',  ( -18.40000000000000213, 64.52132590001231449, -145.7978007008650252 ) ) ;
#253057=CARTESIAN_POINT ( 'NONE',  ( 15.31784899511108655, 66.60336962369454739, -152.1160500917061427 ) ) ;
#253181=DIRECTION ( 'NONE',  ( 0.000000000000000000, -1.000000000000000000, -6.982962677686266711E-15 ) ) ;
#253182=DIRECTION ( 'NONE',  ( -1.000000000000000000, 0.000000000000000000, 0.000000000000000000 ) ) ;
#253215=ORIENTED_EDGE ( 'NONE', *, *, #134582, .F. ) ;
#253598=CARTESIAN_POINT ( 'NONE',  ( 16.87683809663750267, 66.05000000001230376, -157.3731074845244393 ) ) ;
#253906=EDGE_CURVE ( 'NONE', #122105, #18925, #48564, .T. ) ;
#253965=DIRECTION ( 'NONE',  ( 1.186688945009010077E-16, 1.000000000000000000, 6.982962677686266711E-15 ) ) ;
#254170=CARTESIAN_POINT ( 'NONE',  ( -21.65000000000000213, 65.95000000001225260, -149.1731074845244223 ) ) ;
#254287=CARTESIAN_POINT ( 'NONE',  ( -17.27223548800608199, 65.65460260867664033, -147.8895013053080731 ) ) ;
#254295=CARTESIAN_POINT ( 'NONE',  ( -12.25000000000000178, 66.15000000001228386, -153.2731074845244166 ) ) ;
#254393=ORIENTED_EDGE ( 'NONE', *, *, #233668, .F. ) ;
#254418=AXIS2_PLACEMENT_3D ( 'NONE', #7694, #209737, #31135 ) ;
#254432=ORIENTED_EDGE ( 'NONE', *, *, #48590, .T. ) ;
#254492=LINE ( 'NONE', #96696, #84676 ) ;
#254594=CARTESIAN_POINT ( 'NONE',  ( 18.39999999999999503, 64.52683809664981140, -157.3731074845244393 ) ) ;
#254639=CARTESIAN_POINT ( 'NONE',  ( -21.65000000000000213, 66.05000000001230376, -157.2731074845244166 ) ) ;
#254732=VERTEX_POINT ( 'NONE', #203826 ) ;
#254806=FILL_AREA_STYLE_COLOUR ( '', #10813 ) ;
#255009=B_SPLINE_CURVE_WITH_KNOTS ( 'NONE', 3,
 ( #173534, #253006, #71827, #230907 ),
 .UNSPECIFIED., .F., .F.,
 ( 4, 4 ),
 ( 0.000000000000000000, 7.713889350930119414E-05 ),
 .UNSPECIFIED. ) ;
#255120=ORIENTED_EDGE ( 'NONE', *, *, #4097, .T. ) ;
#255265=CARTESIAN_POINT ( 'NONE',  ( -16.94389599337535657, 66.00880201025550775, -149.1307522863228314 ) ) ;
#255622=CARTESIAN_POINT ( 'NONE',  ( 13.54556439290363556, 66.54940788787858708, -154.9669191657160638 ) ) ;
#255739=CARTESIAN_POINT ( 'NONE',  ( -16.83794479845801462, 66.07364258066074569, -149.3266627803021152 ) ) ;
#255861=FACE_OUTER_BOUND ( 'NONE', #114259, .T. ) ;
#256046=CARTESIAN_POINT ( 'NONE',  ( -16.92570016628985385, 66.04121104227242256, -157.4024568144854470 ) ) ;
#256195=ORIENTED_EDGE ( 'NONE', *, *, #185926, .F. ) ;
#256215=ORIENTED_EDGE ( 'NONE', *, *, #157523, .F. ) ;
#256238=AXIS2_PLACEMENT_3D ( 'NONE', #86485, #6975, #241738 ) ;
#256607=CARTESIAN_POINT ( 'NONE',  ( -16.89268316805466341, 66.04827818677011919, -157.3788599630699707 ) ) ;
#256675=ORIENTED_EDGE ( 'NONE', *, *, #76645, .F. ) ;
#256690=CARTESIAN_POINT ( 'NONE',  ( -16.86337532320261090, 66.02003279578788408, -149.0741830155416210 ) ) ;
#256693=ORIENTED_EDGE ( 'NONE', *, *, #48590, .F. ) ;
#256751=FACE_OUTER_BOUND ( 'NONE', #211937, .T. ) ;
#256807=CARTESIAN_POINT ( 'NONE',  ( -16.27683809663751191, 66.65000000001234071, -160.7731074845244450 ) ) ;
#256925=ORIENTED_EDGE ( 'NONE', *, *, #36961, .T. ) ;
#257019=CARTESIAN_POINT ( 'NONE',  ( -16.83199318825828072, 66.06935387203108689, -149.2955222963152266 ) ) ;
#257031=AXIS2_PLACEMENT_3D ( 'NONE', #87585, #207574, #69346 ) ;
#257036=CARTESIAN_POINT ( 'NONE',  ( -12.25000000000000178, 66.65000000001228386, -153.2731074845244166 ) ) ;
#257131=CARTESIAN_POINT ( 'NONE',  ( 15.74999999999999645, 66.15000000001228386, -153.2731074845244450 ) ) ;
#257266=CARTESIAN_POINT ( 'NONE',  ( -18.40000000000000213, 70.35000000001222986, -145.7731074845243882 ) ) ;
#257375=AXIS2_PLACEMENT_3D ( 'NONE', #175846, #14212, #72910 ) ;
#257460=EDGE_CURVE ( 'NONE', #257702, #16882, #15884, .T. ) ;
#257481=CARTESIAN_POINT ( 'NONE',  ( -18.40000000000000213, 64.25000000001224976, -149.1731074845244507 ) ) ;
#257588=VERTEX_POINT ( 'NONE', #183910 ) ;
#257702=VERTEX_POINT ( 'NONE', #149942 ) ;
#257720=ADVANCED_FACE ( 'NONE', ( #148653 ), #224488, .T. ) ;
#257738=CARTESIAN_POINT ( 'NONE',  ( 18.39999999999999503, 64.25000000001222134, -145.7731074845244450 ) ) ;
#257833=CARTESIAN_POINT ( 'NONE',  ( -16.90987985657660886, 66.04219248183250102, -149.1538203956407926 ) ) ;
ENDSEC;
END-ISO-10303-21;
